ISO-10303-21;
HEADER;
FILE_DESCRIPTION (('STEP AP214'),
    '1' );
FILE_NAME ('10. Furnel.step',
    '2026-10-09T14:04:53',
    ( '' ),
    ( '' ),
    'SwSTEP 2.0',
    'SolidWorks 2021',
    '' );
FILE_SCHEMA (( 'AUTOMOTIVE_DESIGN' ));
ENDSEC;

DATA;
#3=FACE_OUTER_BOUND ( 'NONE', #81469, .T. ) ;
#43=VERTEX_POINT ( 'NONE', #19085 ) ;
#133=AXIS2_PLACEMENT_3D ( 'NONE', #79588, #64998, #88226 ) ;
#160=VERTEX_POINT ( 'NONE', #69724 ) ;
#188=AXIS2_PLACEMENT_3D ( 'NONE', #4644, #61834, #45635 ) ;
#306=MECHANICAL_DESIGN_GEOMETRIC_PRESENTATION_REPRESENTATION('',(#93377),#55528);
#609=EDGE_CURVE ( 'NONE', #31239, #105636, #64688, .T. ) ;
#637=ADVANCED_FACE ( 'NONE', ( #97560 ), #104603, .F. ) ;
#827=UNCERTAINTY_MEASURE_WITH_UNIT (LENGTH_MEASURE( 1.000000000000000082E-05 ), #38778, 'distance_accuracy_value', 'NONE');
#885=AXIS2_PLACEMENT_3D ( 'NONE', #85043, #45132, #44050 ) ;
#893=FILL_AREA_STYLE ('',( #24711 ) ) ;
#1015=AXIS2_PLACEMENT_3D ( 'NONE', #67823, #84544, #17683 ) ;
#1076=DIRECTION ( 'NONE',  ( 0.000000000000000000, 1.000000000000000000, 0.000000000000000000 ) ) ;
#1084=VERTEX_POINT ( 'NONE', #98506 ) ;
#1113=EDGE_CURVE ( 'NONE', #66070, #72821, #25654, .T. ) ;
#1115=LINE ( 'NONE', #90159, #104394 ) ;
#1162=DIRECTION ( 'NONE',  ( 0.000000000000000000, 1.000000000000000000, 0.000000000000000000 ) ) ;
#1198=EDGE_CURVE ( 'NONE', #1084, #96013, #16742, .T. ) ;
#1217=( LENGTH_UNIT ( ) NAMED_UNIT ( * ) SI_UNIT ( .MILLI., .METRE. ) );
#1219=CIRCLE ( 'NONE', #23690, 60.00000000000000000 ) ;
#1251=CARTESIAN_POINT ( 'NONE',  ( 1.890187507280920418E-15, -1.000000000000000000, -15.43455230191221261 ) ) ;
#1283=ORIENTED_EDGE ( 'NONE', *, *, #100237, .T. ) ;
#1307=AXIS2_PLACEMENT_3D ( 'NONE', #37456, #37990, #86531 ) ;
#1453=CARTESIAN_POINT ( 'NONE',  ( 0.000000000000000000, 50.00000000000000000, 0.000000000000000000 ) ) ;
#1490=EDGE_CURVE ( 'NONE', #80282, #84910, #59881, .T. ) ;
#1494=DIRECTION ( 'NONE',  ( 0.000000000000000000, 0.000000000000000000, 1.000000000000000000 ) ) ;
#1497=STYLED_ITEM ( 'NONE', ( #106107 ), #89707 ) ;
#1507=VERTEX_POINT ( 'NONE', #87137 ) ;
#1549=FACE_OUTER_BOUND ( 'NONE', #26116, .T. ) ;
#1660=CIRCLE ( 'NONE', #84139, 56.85174851683467523 ) ;
#1680=UNCERTAINTY_MEASURE_WITH_UNIT (LENGTH_MEASURE( 1.000000000000000082E-05 ), #104797, 'distance_accuracy_value', 'NONE');
#1691=CARTESIAN_POINT ( 'NONE',  ( 0.000000000000000000, 0.1588408748199928722, 0.000000000000000000 ) ) ;
#1704=EDGE_LOOP ( 'NONE', ( #80984, #96917, #80755, #5682 ) ) ;
#1802=VERTEX_POINT ( 'NONE', #20599 ) ;
#1907=ADVANCED_FACE ( 'NONE', ( #15610 ), #71948, .T. ) ;
#1920=ORIENTED_EDGE ( 'NONE', *, *, #50012, .T. ) ;
#1998=DIRECTION ( 'NONE',  ( 0.000000000000000000, 1.000000000000000000, 0.000000000000000000 ) ) ;
#2095=CARTESIAN_POINT ( 'NONE',  ( 0.000000000000000000, 44.50000000000000711, 0.000000000000000000 ) ) ;
#2232=EDGE_CURVE ( 'NONE', #73687, #37488, #32403, .T. ) ;
#2293=SURFACE_STYLE_USAGE ( .BOTH. , #69195 ) ;
#2314=ORIENTED_EDGE ( 'NONE', *, *, #20001, .T. ) ;
#2359=ORIENTED_EDGE ( 'NONE', *, *, #9804, .T. ) ;
#2477=UNCERTAINTY_MEASURE_WITH_UNIT (LENGTH_MEASURE( 1.000000000000000082E-05 ), #87426, 'distance_accuracy_value', 'NONE');
#2523=( NAMED_UNIT ( * ) SI_UNIT ( $, .STERADIAN. ) SOLID_ANGLE_UNIT ( ) );
#2538=CARTESIAN_POINT ( 'NONE',  ( 0.000000000000000000, 48.50000000000000000, 0.000000000000000000 ) ) ;
#2579=VERTEX_POINT ( 'NONE', #55799 ) ;
#2609=MECHANICAL_DESIGN_GEOMETRIC_PRESENTATION_REPRESENTATION('',(#33593),#16398);
#2629=ORIENTED_EDGE ( 'NONE', *, *, #84130, .T. ) ;
#2635=FACE_OUTER_BOUND ( 'NONE', #40239, .T. ) ;
#2665=CIRCLE ( 'NONE', #13045, 60.50000000000000000 ) ;
#2786=FACE_BOUND ( 'NONE', #70567, .T. ) ;
#2862=DIRECTION ( 'NONE',  ( 0.000000000000000000, 1.000000000000000000, 0.000000000000000000 ) ) ;
#2871=DIRECTION ( 'NONE',  ( 1.224646799147353700E-16, 0.000000000000000000, -1.000000000000000000 ) ) ;
#3157=ORIENTED_EDGE ( 'NONE', *, *, #98683, .F. ) ;
#3309=CARTESIAN_POINT ( 'NONE',  ( 0.000000000000000000, 50.50000000000000000, 0.000000000000000000 ) ) ;
#3431=CARTESIAN_POINT ( 'NONE',  ( 0.000000000000000000, 79.50000000000000000, 0.000000000000000000 ) ) ;
#3617=CARTESIAN_POINT ( 'NONE',  ( 0.000000000000000000, 80.00000000000000000, 0.000000000000000000 ) ) ;
#3809=AXIS2_PLACEMENT_3D ( 'NONE', #79098, #5221, #61344 ) ;
#3836=EDGE_LOOP ( 'NONE', ( #20379, #94806 ) ) ;
#3936=EDGE_LOOP ( 'NONE', ( #51030, #14680, #30824, #22393 ) ) ;
#4030=CARTESIAN_POINT ( 'NONE',  ( 0.000000000000000000, 79.50000000000000000, 65.00000000000000000 ) ) ;
#4136=VECTOR ( 'NONE', #72568, 1000.000000000000000 ) ;
#4210=( LENGTH_UNIT ( ) NAMED_UNIT ( * ) SI_UNIT ( .MILLI., .METRE. ) );
#4216=DIRECTION ( 'NONE',  ( 0.000000000000000000, 1.000000000000000000, 0.000000000000000000 ) ) ;
#4417=EDGE_CURVE ( 'NONE', #28073, #21338, #103411, .T. ) ;
#4432=DIRECTION ( 'NONE',  ( 0.000000000000000000, 0.000000000000000000, 1.000000000000000000 ) ) ;
#4441=CIRCLE ( 'NONE', #14750, 66.00000000000000000 ) ;
#4560=CIRCLE ( 'NONE', #18359, 0.5000000000000004441 ) ;
#4571=CARTESIAN_POINT ( 'NONE',  ( 0.000000000000000000, 44.00000000000000711, 0.000000000000000000 ) ) ;
#4644=CARTESIAN_POINT ( 'NONE',  ( 0.000000000000000000, 48.50000000000000000, 0.000000000000000000 ) ) ;
#4654=CARTESIAN_POINT ( 'NONE',  ( 0.000000000000000000, 80.00000000000000000, 0.000000000000000000 ) ) ;
#4802=ORIENTED_EDGE ( 'NONE', *, *, #20430, .T. ) ;
#4804=DIRECTION ( 'NONE',  ( 1.000000000000000000, -0.000000000000000000, 1.224646799147353207E-16 ) ) ;
#4815=STYLED_ITEM ( 'NONE', ( #22145 ), #1907 ) ;
#4916=DIRECTION ( 'NONE',  ( 0.000000000000000000, 1.000000000000000000, 0.000000000000000000 ) ) ;
#4928=AXIS2_PLACEMENT_3D ( 'NONE', #88509, #13000, #71766 ) ;
#4970=FACE_OUTER_BOUND ( 'NONE', #26918, .T. ) ;
#5133=CARTESIAN_POINT ( 'NONE',  ( 0.000000000000000000, 0.000000000000000000, 0.000000000000000000 ) ) ;
#5148=ORIENTED_EDGE ( 'NONE', *, *, #90673, .T. ) ;
#5160=DIRECTION ( 'NONE',  ( 0.000000000000000000, 0.000000000000000000, -1.000000000000000000 ) ) ;
#5221=DIRECTION ( 'NONE',  ( 0.000000000000000000, 1.000000000000000000, 0.000000000000000000 ) ) ;
#5233=CARTESIAN_POINT ( 'NONE',  ( 1.971262872859045587E-15, -1.023477375540016387, -16.09658290236430389 ) ) ;
#5314=DIRECTION ( 'NONE',  ( 0.000000000000000000, 1.000000000000000000, 0.000000000000000000 ) ) ;
#5345=DIRECTION ( 'NONE',  ( 0.000000000000000000, 0.000000000000000000, 1.000000000000000000 ) ) ;
#5411=MECHANICAL_DESIGN_GEOMETRIC_PRESENTATION_REPRESENTATION('',(#19247),#86429);
#5425=AXIS2_PLACEMENT_3D ( 'NONE', #70060, #37736, #37193 ) ;
#5464=CARTESIAN_POINT ( 'NONE',  ( 0.000000000000000000, 50.50000000000000000, 0.000000000000000000 ) ) ;
#5524=ORIENTED_EDGE ( 'NONE', *, *, #23404, .F. ) ;
#5558=AXIS2_PLACEMENT_3D ( 'NONE', #1453, #34417, #99632 ) ;
#5592=CIRCLE ( 'NONE', #65867, 15.14825148316532832 ) ;
#5661=LINE ( 'NONE', #71990, #36097 ) ;
#5682=ORIENTED_EDGE ( 'NONE', *, *, #90673, .F. ) ;
#5689=ORIENTED_EDGE ( 'NONE', *, *, #57577, .F. ) ;
#5694=DIRECTION ( 'NONE',  ( 0.000000000000000000, 1.000000000000000000, 0.000000000000000000 ) ) ;
#5709=( GEOMETRIC_REPRESENTATION_CONTEXT ( 3 ) GLOBAL_UNCERTAINTY_ASSIGNED_CONTEXT ( ( #26283 ) ) GLOBAL_UNIT_ASSIGNED_CONTEXT ( ( #61897, #102865, #13832 ) ) REPRESENTATION_CONTEXT ( 'NONE', 'WORKASPACE' ) );
#5713=STYLED_ITEM ( 'NONE', ( #84298 ), #52429 ) ;
#5717=ORIENTED_EDGE ( 'NONE', *, *, #90616, .F. ) ;
#5770=CARTESIAN_POINT ( 'NONE',  ( 7.531577814756222656E-15, 44.00000000000000711, -61.50000000000000000 ) ) ;
#5853=FILL_AREA_STYLE_COLOUR ( '', #63048 ) ;
#5921=( NAMED_UNIT ( * ) PLANE_ANGLE_UNIT ( ) SI_UNIT ( $, .RADIAN. ) );
#5939=SURFACE_STYLE_FILL_AREA ( #88478 ) ;
#6003=FILL_AREA_STYLE ('',( #97658 ) ) ;
#6009=UNCERTAINTY_MEASURE_WITH_UNIT (LENGTH_MEASURE( 1.000000000000000082E-05 ), #86345, 'distance_accuracy_value', 'NONE');
#6068=VERTEX_POINT ( 'NONE', #106676 ) ;
#6122=AXIS2_PLACEMENT_3D ( 'NONE', #78826, #64775, #46473 ) ;
#6172=DIRECTION ( 'NONE',  ( 0.000000000000000000, 0.000000000000000000, 1.000000000000000000 ) ) ;
#6216=CARTESIAN_POINT ( 'NONE',  ( 0.000000000000000000, 43.34115912517999902, 57.50357696970298349 ) ) ;
#6256=DIRECTION ( 'NONE',  ( 0.000000000000000000, 0.000000000000000000, -1.000000000000000000 ) ) ;
#6272=ORIENTED_EDGE ( 'NONE', *, *, #51398, .F. ) ;
#6277=SURFACE_STYLE_FILL_AREA ( #52317 ) ;
#6318=ORIENTED_EDGE ( 'NONE', *, *, #28723, .T. ) ;
#6529=SURFACE_SIDE_STYLE ('',( #54538 ) ) ;
#6583=CARTESIAN_POINT ( 'NONE',  ( 0.000000000000000000, 48.00000000000000000, 0.000000000000000000 ) ) ;
#6624=CARTESIAN_POINT ( 'NONE',  ( 0.000000000000000000, 49.00000000000000000, 0.000000000000000000 ) ) ;
#6626=DIRECTION ( 'NONE',  ( 0.000000000000000000, 1.000000000000000000, 0.000000000000000000 ) ) ;
#6833=ORIENTED_EDGE ( 'NONE', *, *, #20025, .F. ) ;
#6894=SURFACE_STYLE_FILL_AREA ( #39816 ) ;
#6974=DIRECTION ( 'NONE',  ( 0.000000000000000000, 0.000000000000000000, 1.000000000000000000 ) ) ;
#7004=( NAMED_UNIT ( * ) PLANE_ANGLE_UNIT ( ) SI_UNIT ( $, .RADIAN. ) );
#7065=ORIENTED_EDGE ( 'NONE', *, *, #89884, .F. ) ;
#7120=STYLED_ITEM ( 'NONE', ( #14905 ), #105482 ) ;
#7172=TOROIDAL_SURFACE ( 'NONE', #55443, 59.50000000000000000, 0.5000000000000000000 ) ;
#7400=CIRCLE ( 'NONE', #67706, 0.5000000000000004441 ) ;
#7410=DIRECTION ( 'NONE',  ( 1.000000000000000000, -0.000000000000000000, 1.224646799147353207E-16 ) ) ;
#7523=DIRECTION ( 'NONE',  ( 0.000000000000000000, 0.000000000000000000, 1.000000000000000000 ) ) ;
#7552=ORIENTED_EDGE ( 'NONE', *, *, #90121, .T. ) ;
#7560=CARTESIAN_POINT ( 'NONE',  ( 0.000000000000000000, 0.000000000000000000, 0.000000000000000000 ) ) ;
#7747=AXIS2_PLACEMENT_3D ( 'NONE', #41901, #32782, #24167 ) ;
#7766=DIRECTION ( 'NONE',  ( 1.224646799147349509E-16, 0.000000000000000000, -1.000000000000000000 ) ) ;
#7780=EDGE_LOOP ( 'NONE', ( #6318, #102256 ) ) ;
#7818=CIRCLE ( 'NONE', #6122, 9.500000000000000000 ) ;
#7887=CONICAL_SURFACE ( 'NONE', #45789, 16.09658290236430389, 0.7509290623979402168 ) ;
#7894=VERTEX_POINT ( 'NONE', #54021 ) ;
#7895=( GEOMETRIC_REPRESENTATION_CONTEXT ( 3 ) GLOBAL_UNCERTAINTY_ASSIGNED_CONTEXT ( ( #827 ) ) GLOBAL_UNIT_ASSIGNED_CONTEXT ( ( #38778, #95951, #94897 ) ) REPRESENTATION_CONTEXT ( 'NONE', 'WORKASPACE' ) );
#8046=( LENGTH_UNIT ( ) NAMED_UNIT ( * ) SI_UNIT ( .MILLI., .METRE. ) );
#8096=AXIS2_PLACEMENT_3D ( 'NONE', #95213, #88702, #54185 ) ;
#8147=AXIS2_PLACEMENT_3D ( 'NONE', #6624, #71894, #62761 ) ;
#8192=ORIENTED_EDGE ( 'NONE', *, *, #51398, .T. ) ;
#8194=AXIS2_PLACEMENT_3D ( 'NONE', #38587, #73436, #70417 ) ;
#8205=CARTESIAN_POINT ( 'NONE',  ( 0.000000000000000000, 43.00000000000000000, 0.000000000000000000 ) ) ;
#8213=ORIENTED_EDGE ( 'NONE', *, *, #36258, .F. ) ;
#8413=CARTESIAN_POINT ( 'NONE',  ( 7.531577814756222656E-15, 48.00000000000000000, -61.50000000000000000 ) ) ;
#8414=EDGE_CURVE ( 'NONE', #41582, #22823, #12166, .T. ) ;
#8453=LINE ( 'NONE', #89909, #21499 ) ;
#8455=DIRECTION ( 'NONE',  ( 0.000000000000000000, 1.000000000000000000, 0.000000000000000000 ) ) ;
#8504=ORIENTED_EDGE ( 'NONE', *, *, #42229, .T. ) ;
#8565=CARTESIAN_POINT ( 'NONE',  ( 0.000000000000000000, 50.50000000000000000, 64.50000000000000000 ) ) ;
#8623=CIRCLE ( 'NONE', #22456, 0.4999999999999987232 ) ;
#8795=CIRCLE ( 'NONE', #5425, 60.00000000000000000 ) ;
#8846=EDGE_LOOP ( 'NONE', ( #19422, #9725, #76243, #73531 ) ) ;
#8869=VERTEX_POINT ( 'NONE', #46793 ) ;
#8993=EDGE_CURVE ( 'NONE', #22326, #19286, #92620, .T. ) ;
#9057=CARTESIAN_POINT ( 'NONE',  ( 0.000000000000000000, -1.000000000000000000, 15.43455230191221261 ) ) ;
#9071=AXIS2_PLACEMENT_3D ( 'NONE', #18840, #92143, #52216 ) ;
#9176=ORIENTED_EDGE ( 'NONE', *, *, #1113, .F. ) ;
#9475=DIRECTION ( 'NONE',  ( 0.000000000000000000, 1.000000000000000000, 0.000000000000000000 ) ) ;
#9641=VERTEX_POINT ( 'NONE', #87283 ) ;
#9725=ORIENTED_EDGE ( 'NONE', *, *, #63645, .F. ) ;
#9788=( NAMED_UNIT ( * ) SI_UNIT ( $, .STERADIAN. ) SOLID_ANGLE_UNIT ( ) );
#9804=EDGE_CURVE ( 'NONE', #83020, #21929, #45726, .T. ) ;
#9834=EDGE_CURVE ( 'NONE', #63571, #97678, #30184, .T. ) ;
#9855=DIRECTION ( 'NONE',  ( 1.224646799147349509E-16, 0.000000000000000000, -1.000000000000000000 ) ) ;
#9859=( NAMED_UNIT ( * ) SI_UNIT ( $, .STERADIAN. ) SOLID_ANGLE_UNIT ( ) );
#9888=AXIS2_PLACEMENT_3D ( 'NONE', #19563, #95525, #29246 ) ;
#9890=CARTESIAN_POINT ( 'NONE',  ( 7.007095409419857340E-15, 44.50000000000000711, -57.21727615095610275 ) ) ;
#10012=ADVANCED_FACE ( 'NONE', ( #69909, #63429 ), #69386, .T. ) ;
#10096=FACE_OUTER_BOUND ( 'NONE', #64238, .T. ) ;
#10257=ORIENTED_EDGE ( 'NONE', *, *, #101306, .F. ) ;
#10331=VERTEX_POINT ( 'NONE', #56344 ) ;
#10421=AXIS2_PLACEMENT_3D ( 'NONE', #70526, #14921, #55378 ) ;
#10499=CARTESIAN_POINT ( 'NONE',  ( 0.000000000000000000, 0.5000000000000000000, 14.78272384904389192 ) ) ;
#10539=EDGE_CURVE ( 'NONE', #74088, #38824, #36675, .T. ) ;
#10594=CIRCLE ( 'NONE', #93293, 61.00000000000000000 ) ;
#10689=EDGE_CURVE ( 'NONE', #160, #77143, #4560, .T. ) ;
#10692=FACE_BOUND ( 'NONE', #75750, .T. ) ;
#10728=AXIS2_PLACEMENT_3D ( 'NONE', #14983, #57033, #47878 ) ;
#10904=DIRECTION ( 'NONE',  ( 0.000000000000000000, 1.000000000000000000, 0.000000000000000000 ) ) ;
#11002=DIRECTION ( 'NONE',  ( -0.000000000000000000, -1.000000000000000000, -0.000000000000000000 ) ) ;
#11052=DIRECTION ( 'NONE',  ( 0.000000000000000000, 1.000000000000000000, 0.000000000000000000 ) ) ;
#11112=EDGE_LOOP ( 'NONE', ( #3157, #33153, #38161, #13120 ) ) ;
#11215=ORIENTED_EDGE ( 'NONE', *, *, #73725, .F. ) ;
#11294=PRODUCT ( '10. Furnel', '10. Furnel', '', ( #49230 ) ) ;
#11307=DIRECTION ( 'NONE',  ( 0.000000000000000000, 0.000000000000000000, -1.000000000000000000 ) ) ;
#11339=ORIENTED_EDGE ( 'NONE', *, *, #4417, .T. ) ;
#11432=CIRCLE ( 'NONE', #61200, 65.00000000000000000 ) ;
#11449=DIRECTION ( 'NONE',  ( 1.000000000000000000, -0.000000000000000000, 1.224646799147353207E-16 ) ) ;
#11476=ORIENTED_EDGE ( 'NONE', *, *, #53800, .T. ) ;
#11544=ORIENTED_EDGE ( 'NONE', *, *, #61853, .F. ) ;
#11565=EDGE_CURVE ( 'NONE', #96013, #1084, #71646, .T. ) ;
#11628=EDGE_CURVE ( 'NONE', #80282, #9641, #8453, .T. ) ;
#11648=ORIENTED_EDGE ( 'NONE', *, *, #85692, .F. ) ;
#11733=ORIENTED_EDGE ( 'NONE', *, *, #17815, .F. ) ;
#11748=AXIS2_PLACEMENT_3D ( 'NONE', #37184, #13385, #38756 ) ;
#11768=ORIENTED_EDGE ( 'NONE', *, *, #89884, .T. ) ;
#11911=AXIS2_PLACEMENT_3D ( 'NONE', #103874, #87713, #101759 ) ;
#11948=SURFACE_STYLE_USAGE ( .BOTH. , #93420 ) ;
#11986=DIRECTION ( 'NONE',  ( -0.000000000000000000, -1.000000000000000000, -0.000000000000000000 ) ) ;
#11996=CARTESIAN_POINT ( 'NONE',  ( 7.347880794884118356E-15, 49.50000000000000000, -60.00000000000000000 ) ) ;
#12082=STYLED_ITEM ( 'NONE', ( #13338 ), #46250 ) ;
#12166=CIRCLE ( 'NONE', #70924, 0.5000000000000004441 ) ;
#12188=DIRECTION ( 'NONE',  ( 0.000000000000000000, -0.000000000000000000, 1.000000000000000000 ) ) ;
#12190=CARTESIAN_POINT ( 'NONE',  ( 0.000000000000000000, 0.000000000000000000, 61.50000000000000000 ) ) ;
#12214=DIRECTION ( 'NONE',  ( 0.000000000000000000, 0.000000000000000000, 1.000000000000000000 ) ) ;
#12287=SURFACE_STYLE_USAGE ( .BOTH. , #21482 ) ;
#12291=CARTESIAN_POINT ( 'NONE',  ( 4.408728476930471644E-15, 0.1588408748199928722, -15.14825148316532832 ) ) ;
#12436=ADVANCED_FACE ( 'NONE', ( #43363 ), #103222, .T. ) ;
#12548=TOROIDAL_SURFACE ( 'NONE', #19546, 14.78272384904389192, 0.5000000000000000000 ) ;
#12582=VERTEX_POINT ( 'NONE', #73455 ) ;
#12588=FILL_AREA_STYLE_COLOUR ( '', #87405 ) ;
#12772=FILL_AREA_STYLE_COLOUR ( '', #97009 ) ;
#12820=DIRECTION ( 'NONE',  ( 0.000000000000000000, -0.000000000000000000, 1.000000000000000000 ) ) ;
#12852=CARTESIAN_POINT ( 'NONE',  ( 0.000000000000000000, 45.50000000000000711, 0.000000000000000000 ) ) ;
#12853=( NAMED_UNIT ( * ) PLANE_ANGLE_UNIT ( ) SI_UNIT ( $, .RADIAN. ) );
#13000=DIRECTION ( 'NONE',  ( 1.000000000000000000, -0.000000000000000000, 1.224646799147353207E-16 ) ) ;
#13027=PRESENTATION_STYLE_ASSIGNMENT (( #79891 ) ) ;
#13043=EDGE_LOOP ( 'NONE', ( #7552, #98787, #13470, #11648 ) ) ;
#13045=AXIS2_PLACEMENT_3D ( 'NONE', #101757, #36009, #20375 ) ;
#13115=PRESENTATION_STYLE_ASSIGNMENT (( #96191 ) ) ;
#13120=ORIENTED_EDGE ( 'NONE', *, *, #14992, .F. ) ;
#13135=CARTESIAN_POINT ( 'NONE',  ( 0.000000000000000000, 49.50000000000000000, 0.000000000000000000 ) ) ;
#13301=STYLED_ITEM ( 'NONE', ( #13115 ), #15930 ) ;
#13338=PRESENTATION_STYLE_ASSIGNMENT (( #12287 ) ) ;
#13359=EDGE_LOOP ( 'NONE', ( #32761, #56534, #104398, #19438 ) ) ;
#13373=AXIS2_PLACEMENT_3D ( 'NONE', #27435, #26373, #1494 ) ;
#13378=EDGE_CURVE ( 'NONE', #87282, #105636, #67990, .T. ) ;
#13385=DIRECTION ( 'NONE',  ( 0.000000000000000000, 1.000000000000000000, 0.000000000000000000 ) ) ;
#13470=ORIENTED_EDGE ( 'NONE', *, *, #46332, .T. ) ;
#13489=CIRCLE ( 'NONE', #75550, 15.80007993603364724 ) ;
#13500=PRESENTATION_STYLE_ASSIGNMENT (( #54477 ) ) ;
#13651=( NAMED_UNIT ( * ) PLANE_ANGLE_UNIT ( ) SI_UNIT ( $, .RADIAN. ) );
#13751=DIRECTION ( 'NONE',  ( 0.000000000000000000, 0.000000000000000000, -1.000000000000000000 ) ) ;
#13784=DIRECTION ( 'NONE',  ( 0.000000000000000000, 1.000000000000000000, 0.000000000000000000 ) ) ;
#13832=( NAMED_UNIT ( * ) SI_UNIT ( $, .STERADIAN. ) SOLID_ANGLE_UNIT ( ) );
#13948=EDGE_CURVE ( 'NONE', #15446, #7894, #26851, .T. ) ;
#13965=DIRECTION ( 'NONE',  ( 1.000000000000000000, -0.000000000000000000, 1.224646799147353207E-16 ) ) ;
#13985=ORIENTED_EDGE ( 'NONE', *, *, #100305, .F. ) ;
#13991=CARTESIAN_POINT ( 'NONE',  ( 7.531577814756222656E-15, 0.000000000000000000, -61.50000000000000000 ) ) ;
#14009=DIRECTION ( 'NONE',  ( -1.000000000000000000, 0.000000000000000000, 0.000000000000000000 ) ) ;
#14029=FACE_OUTER_BOUND ( 'NONE', #55580, .T. ) ;
#14353=SURFACE_STYLE_FILL_AREA ( #104439 ) ;
#14385=DIRECTION ( 'NONE',  ( 0.000000000000000000, 1.000000000000000000, 0.000000000000000000 ) ) ;
#14387=EDGE_LOOP ( 'NONE', ( #23283, #48214, #99153, #86269 ) ) ;
#14534=DIRECTION ( 'NONE',  ( 0.000000000000000000, 1.000000000000000000, 0.000000000000000000 ) ) ;
#14542=ORIENTED_EDGE ( 'NONE', *, *, #87679, .F. ) ;
#14666=FACE_OUTER_BOUND ( 'NONE', #53405, .T. ) ;
#14680=ORIENTED_EDGE ( 'NONE', *, *, #67180, .T. ) ;
#14729=DIRECTION ( 'NONE',  ( 0.000000000000000000, 0.000000000000000000, 1.000000000000000000 ) ) ;
#14750=AXIS2_PLACEMENT_3D ( 'NONE', #31729, #64616, #97483 ) ;
#14834=ORIENTED_EDGE ( 'NONE', *, *, #19819, .T. ) ;
#14905=PRESENTATION_STYLE_ASSIGNMENT (( #27569 ) ) ;
#14921=DIRECTION ( 'NONE',  ( 0.000000000000000000, 1.000000000000000000, 0.000000000000000000 ) ) ;
#14939=VERTEX_POINT ( 'NONE', #25840 ) ;
#14958=EDGE_LOOP ( 'NONE', ( #76945, #15199, #11476, #71700 ) ) ;
#14983=CARTESIAN_POINT ( 'NONE',  ( 0.000000000000000000, 0.000000000000000000, 0.000000000000000000 ) ) ;
#14992=EDGE_CURVE ( 'NONE', #31239, #2579, #63150, .T. ) ;
#15179=ORIENTED_EDGE ( 'NONE', *, *, #38730, .F. ) ;
#15199=ORIENTED_EDGE ( 'NONE', *, *, #66432, .F. ) ;
#15212=CARTESIAN_POINT ( 'NONE',  ( 0.000000000000000000, 49.50000000000000000, 0.000000000000000000 ) ) ;
#15257=AXIS2_PLACEMENT_3D ( 'NONE', #104626, #14009, #31822 ) ;
#15298=CIRCLE ( 'NONE', #35996, 0.5000000000000004441 ) ;
#15446=VERTEX_POINT ( 'NONE', #93464 ) ;
#15556=VECTOR ( 'NONE', #5694, 1000.000000000000000 ) ;
#15606=CARTESIAN_POINT ( 'NONE',  ( 0.000000000000000000, 43.50000000000000711, 0.000000000000000000 ) ) ;
#15610=FACE_OUTER_BOUND ( 'NONE', #14958, .T. ) ;
#15688=DIRECTION ( 'NONE',  ( 0.000000000000000000, 0.000000000000000000, 1.000000000000000000 ) ) ;
#15708=TOROIDAL_SURFACE ( 'NONE', #21009, 9.000000000000000000, 0.5000000000000000000 ) ;
#15788=EDGE_LOOP ( 'NONE', ( #105525, #85735, #28213, #71402 ) ) ;
#15930=ADVANCED_FACE ( 'NONE', ( #30404 ), #46057, .T. ) ;
#15947=ORIENTED_EDGE ( 'NONE', *, *, #10689, .F. ) ;
#16099=COLOUR_RGB ( '', 0.66274510, 0.83137255, 0.94901961) ;
#16398=( GEOMETRIC_REPRESENTATION_CONTEXT ( 3 ) GLOBAL_UNCERTAINTY_ASSIGNED_CONTEXT ( ( #18563 ) ) GLOBAL_UNIT_ASSIGNED_CONTEXT ( ( #104499, #30647, #48380 ) ) REPRESENTATION_CONTEXT ( 'NONE', 'WORKASPACE' ) );
#16522=AXIS2_PLACEMENT_3D ( 'NONE', #99005, #24638, #25170 ) ;
#16541=DIRECTION ( 'NONE',  ( 0.000000000000000000, 1.000000000000000000, 0.000000000000000000 ) ) ;
#16586=( LENGTH_UNIT ( ) NAMED_UNIT ( * ) SI_UNIT ( .MILLI., .METRE. ) );
#16591=SURFACE_STYLE_USAGE ( .BOTH. , #57035 ) ;
#16600=ORIENTED_EDGE ( 'NONE', *, *, #53947, .F. ) ;
#16742=CIRCLE ( 'NONE', #16999, 64.50000000000000000 ) ;
#16809=CARTESIAN_POINT ( 'NONE',  ( 0.000000000000000000, 80.00000000000000000, 0.000000000000000000 ) ) ;
#16865=COLOUR_RGB ( '', 0.72549020, 0.75294118, 0.79215686) ;
#16999=AXIS2_PLACEMENT_3D ( 'NONE', #51008, #18152, #83390 ) ;
#17140=CARTESIAN_POINT ( 'NONE',  ( 0.000000000000000000, -14.49999999999999822, 0.000000000000000000 ) ) ;
#17366=DIRECTION ( 'NONE',  ( 0.000000000000000000, 0.000000000000000000, 1.000000000000000000 ) ) ;
#17626=AXIS2_PLACEMENT_3D ( 'NONE', #86968, #11986, #4432 ) ;
#17683=DIRECTION ( 'NONE',  ( 0.000000000000000000, 0.000000000000000000, 1.000000000000000000 ) ) ;
#17720=AXIS2_PLACEMENT_3D ( 'NONE', #92684, #51685, #84605 ) ;
#17742=( GEOMETRIC_REPRESENTATION_CONTEXT ( 3 ) GLOBAL_UNCERTAINTY_ASSIGNED_CONTEXT ( ( #26675 ) ) GLOBAL_UNIT_ASSIGNED_CONTEXT ( ( #58357, #57272, #9788 ) ) REPRESENTATION_CONTEXT ( 'NONE', 'WORKASPACE' ) );
#17773=EDGE_CURVE ( 'NONE', #92669, #94251, #72995, .T. ) ;
#17815=EDGE_CURVE ( 'NONE', #21876, #6068, #26570, .T. ) ;
#17866=PLANE ( 'NONE',  #61646 ) ;
#17870=DIRECTION ( 'NONE',  ( -0.000000000000000000, -1.000000000000000000, -0.000000000000000000 ) ) ;
#17983=( NAMED_UNIT ( * ) PLANE_ANGLE_UNIT ( ) SI_UNIT ( $, .RADIAN. ) );
#18050=ORIENTED_EDGE ( 'NONE', *, *, #65794, .T. ) ;
#18114=COLOUR_RGB ( '', 0.66274510, 0.83137255, 0.94901961) ;
#18152=DIRECTION ( 'NONE',  ( 0.000000000000000000, 1.000000000000000000, 0.000000000000000000 ) ) ;
#18214=SURFACE_STYLE_FILL_AREA ( #893 ) ;
#18231=( NAMED_UNIT ( * ) PLANE_ANGLE_UNIT ( ) SI_UNIT ( $, .RADIAN. ) );
#18359=AXIS2_PLACEMENT_3D ( 'NONE', #96187, #64353, #55162 ) ;
#18563=UNCERTAINTY_MEASURE_WITH_UNIT (LENGTH_MEASURE( 1.000000000000000082E-05 ), #104499, 'distance_accuracy_value', 'NONE');
#18581=DIRECTION ( 'NONE',  ( 0.000000000000000000, 1.000000000000000000, 0.000000000000000000 ) ) ;
#18655=STYLED_ITEM ( 'NONE', ( #60569 ), #59080 ) ;
#18755=DIRECTION ( 'NONE',  ( 0.000000000000000000, 0.000000000000000000, 1.000000000000000000 ) ) ;
#18758=CIRCLE ( 'NONE', #25611, 0.5000000000000004441 ) ;
#18840=CARTESIAN_POINT ( 'NONE',  ( 0.000000000000000000, -0.5000000000000000000, 8.500000000000000000 ) ) ;
#18846=EDGE_LOOP ( 'NONE', ( #86724, #75867 ) ) ;
#18898=EDGE_LOOP ( 'NONE', ( #34128, #37497 ) ) ;
#19009=COLOUR_RGB ( '', 0.72549020, 0.75294118, 0.79215686) ;
#19076=CARTESIAN_POINT ( 'NONE',  ( 0.000000000000000000, 0.5000000000000000000, 0.000000000000000000 ) ) ;
#19085=CARTESIAN_POINT ( 'NONE',  ( 0.000000000000000000, 45.00000000000000711, 57.21727615095610275 ) ) ;
#19127=FACE_OUTER_BOUND ( 'NONE', #72231, .T. ) ;
#19162=CARTESIAN_POINT ( 'NONE',  ( 0.000000000000000000, 48.00000000000000000, 61.50000000000000000 ) ) ;
#19247=STYLED_ITEM ( 'NONE', ( #106653 ), #82163 ) ;
#19286=VERTEX_POINT ( 'NONE', #82450 ) ;
#19314=( NAMED_UNIT ( * ) PLANE_ANGLE_UNIT ( ) SI_UNIT ( $, .RADIAN. ) );
#19319=FACE_BOUND ( 'NONE', #18898, .T. ) ;
#19332=FILL_AREA_STYLE_COLOUR ( '', #46838 ) ;
#19422=ORIENTED_EDGE ( 'NONE', *, *, #8414, .F. ) ;
#19438=ORIENTED_EDGE ( 'NONE', *, *, #98033, .F. ) ;
#19472=TOROIDAL_SURFACE ( 'NONE', #79706, 57.86910460382442523, 0.5000000000000000000 ) ;
#19507=ORIENTED_EDGE ( 'NONE', *, *, #94232, .F. ) ;
#19546=AXIS2_PLACEMENT_3D ( 'NONE', #19076, #36326, #26115 ) ;
#19562=PLANE ( 'NONE',  #81011 ) ;
#19563=CARTESIAN_POINT ( 'NONE',  ( 0.000000000000000000, 45.00000000000000711, 0.000000000000000000 ) ) ;
#19574=( NAMED_UNIT ( * ) PLANE_ANGLE_UNIT ( ) SI_UNIT ( $, .RADIAN. ) );
#19602=ADVANCED_FACE ( 'NONE', ( #64044 ), #26102, .F. ) ;
#19688=( LENGTH_UNIT ( ) NAMED_UNIT ( * ) SI_UNIT ( .MILLI., .METRE. ) );
#19704=ORIENTED_EDGE ( 'NONE', *, *, #21526, .F. ) ;
#19819=EDGE_CURVE ( 'NONE', #21338, #1507, #62334, .T. ) ;
#19825=ADVANCED_FACE ( 'NONE', ( #87661 ), #7172, .F. ) ;
#19975=COLOUR_RGB ( '', 0.66274510, 0.83137255, 0.94901961) ;
#19983=ADVANCED_FACE ( 'NONE', ( #38979 ), #24474, .T. ) ;
#20001=EDGE_CURVE ( 'NONE', #75344, #43310, #77879, .T. ) ;
#20013=DIRECTION ( 'NONE',  ( 0.000000000000000000, 0.000000000000000000, -1.000000000000000000 ) ) ;
#20025=EDGE_CURVE ( 'NONE', #28073, #54015, #27951, .T. ) ;
#20134=FILL_AREA_STYLE ('',( #43823 ) ) ;
#20195=CARTESIAN_POINT ( 'NONE',  ( 8.143901214329899974E-15, 49.00000000000000000, -66.50000000000000000 ) ) ;
#20203=CIRCLE ( 'NONE', #97572, 8.500000000000000000 ) ;
#20375=DIRECTION ( 'NONE',  ( 0.000000000000000000, 0.000000000000000000, 1.000000000000000000 ) ) ;
#20379=ORIENTED_EDGE ( 'NONE', *, *, #1198, .T. ) ;
#20381=CARTESIAN_POINT ( 'NONE',  ( 0.000000000000000000, 48.00000000000000000, 0.000000000000000000 ) ) ;
#20430=EDGE_CURVE ( 'NONE', #66070, #21786, #52058, .T. ) ;
#20599=CARTESIAN_POINT ( 'NONE',  ( 1.040949779275250140E-15, 0.000000000000000000, -8.500000000000000000 ) ) ;
#20609=CIRCLE ( 'NONE', #63597, 8.000000000000000000 ) ;
#20662=CARTESIAN_POINT ( 'NONE',  ( 0.000000000000000000, 45.50000000000000711, 59.50000000000000000 ) ) ;
#20711=AXIS2_PLACEMENT_3D ( 'NONE', #49983, #98532, #34909 ) ;
#20754=ORIENTED_EDGE ( 'NONE', *, *, #8414, .T. ) ;
#20757=FILL_AREA_STYLE ('',( #12588 ) ) ;
#20776=AXIS2_PLACEMENT_3D ( 'NONE', #57514, #48888, #90977 ) ;
#20943=ADVANCED_FACE ( 'NONE', ( #87030 ), #19472, .F. ) ;
#20984=PLANE ( 'NONE',  #65464 ) ;
#21008=FACE_BOUND ( 'NONE', #82445, .T. ) ;
#21009=AXIS2_PLACEMENT_3D ( 'NONE', #17140, #41926, #24189 ) ;
#21138=DIRECTION ( 'NONE',  ( 0.000000000000000000, 0.000000000000000000, -1.000000000000000000 ) ) ;
#21158=EDGE_LOOP ( 'NONE', ( #69367, #90421, #72732, #23099 ) ) ;
#21163=FILL_AREA_STYLE ('',( #79343 ) ) ;
#21186=CIRCLE ( 'NONE', #83271, 0.5000000000000004441 ) ;
#21187=ORIENTED_EDGE ( 'NONE', *, *, #28723, .F. ) ;
#21193=DIRECTION ( 'NONE',  ( -1.224646799147353454E-16, 0.000000000000000000, -1.000000000000000000 ) ) ;
#21225=CARTESIAN_POINT ( 'NONE',  ( 0.000000000000000000, 43.50000000000000711, -56.99999999999999289 ) ) ;
#21338=VERTEX_POINT ( 'NONE', #53332 ) ;
#21345=DIRECTION ( 'NONE',  ( -0.000000000000000000, -1.000000000000000000, -0.000000000000000000 ) ) ;
#21411=EDGE_CURVE ( 'NONE', #21786, #12582, #7400, .T. ) ;
#21452=DIRECTION ( 'NONE',  ( 0.000000000000000000, 1.000000000000000000, 0.000000000000000000 ) ) ;
#21482=SURFACE_SIDE_STYLE ('',( #45729 ) ) ;
#21495=CARTESIAN_POINT ( 'NONE',  ( 0.000000000000000000, 44.00000000000000711, 0.000000000000000000 ) ) ;
#21499=VECTOR ( 'NONE', #41353, 1000.000000000000000 ) ;
#21526=EDGE_CURVE ( 'NONE', #91723, #59944, #83237, .T. ) ;
#21548=AXIS2_PLACEMENT_3D ( 'NONE', #77631, #4804, #77093 ) ;
#21563=CARTESIAN_POINT ( 'NONE',  ( 0.000000000000000000, 0.000000000000000000, 0.000000000000000000 ) ) ;
#21655=VECTOR ( 'NONE', #39286, 1000.000000000000000 ) ;
#21703=( LENGTH_UNIT ( ) NAMED_UNIT ( * ) SI_UNIT ( .MILLI., .METRE. ) );
#21758=DIRECTION ( 'NONE',  ( -0.000000000000000000, -1.000000000000000000, -0.000000000000000000 ) ) ;
#21784=ADVANCED_FACE ( 'NONE', ( #35865 ), #24753, .T. ) ;
#21786=VERTEX_POINT ( 'NONE', #70848 ) ;
#21787=DIRECTION ( 'NONE',  ( 0.000000000000000000, 1.000000000000000000, 0.000000000000000000 ) ) ;
#21862=EDGE_CURVE ( 'NONE', #59944, #38219, #59456, .T. ) ;
#21875=DIRECTION ( 'NONE',  ( 0.000000000000000000, 0.000000000000000000, 1.000000000000000000 ) ) ;
#21876=VERTEX_POINT ( 'NONE', #47082 ) ;
#21929=VERTEX_POINT ( 'NONE', #40291 ) ;
#22007=DIRECTION ( 'NONE',  ( 0.000000000000000000, 0.000000000000000000, 1.000000000000000000 ) ) ;
#22020=FILL_AREA_STYLE_COLOUR ( '', #18114 ) ;
#22061=CARTESIAN_POINT ( 'NONE',  ( 0.000000000000000000, 0.000000000000000000, 14.78272384904389192 ) ) ;
#22145=PRESENTATION_STYLE_ASSIGNMENT (( #39384 ) ) ;
#22229=ORIENTED_EDGE ( 'NONE', *, *, #90307, .T. ) ;
#22324=DIRECTION ( 'NONE',  ( 0.000000000000000000, 0.000000000000000000, 1.000000000000000000 ) ) ;
#22326=VERTEX_POINT ( 'NONE', #35428 ) ;
#22393=ORIENTED_EDGE ( 'NONE', *, *, #4417, .F. ) ;
#22456=AXIS2_PLACEMENT_3D ( 'NONE', #9057, #41436, #98601 ) ;
#22500=SURFACE_STYLE_USAGE ( .BOTH. , #64008 ) ;
#22522=DIRECTION ( 'NONE',  ( 0.000000000000000000, 0.000000000000000000, 1.000000000000000000 ) ) ;
#22567=PRESENTATION_STYLE_ASSIGNMENT (( #97460 ) ) ;
#22580=DIRECTION ( 'NONE',  ( -0.000000000000000000, -1.000000000000000000, -0.000000000000000000 ) ) ;
#22592=DIRECTION ( 'NONE',  ( 0.000000000000000000, 1.000000000000000000, 0.000000000000000000 ) ) ;
#22604=EDGE_CURVE ( 'NONE', #41058, #72311, #88773, .T. ) ;
#22664=CARTESIAN_POINT ( 'NONE',  ( 0.000000000000000000, 49.00000000000000000, 66.50000000000000000 ) ) ;
#22704=( NAMED_UNIT ( * ) SI_UNIT ( $, .STERADIAN. ) SOLID_ANGLE_UNIT ( ) );
#22738=DIRECTION ( 'NONE',  ( -0.000000000000000000, -1.000000000000000000, -0.000000000000000000 ) ) ;
#22742=ORIENTED_EDGE ( 'NONE', *, *, #50278, .T. ) ;
#22756=CIRCLE ( 'NONE', #5558, 60.50000000000000000 ) ;
#22765=TOROIDAL_SURFACE ( 'NONE', #3809, 15.43455230191221261, 0.5000000000000000000 ) ;
#22823=VERTEX_POINT ( 'NONE', #20195 ) ;
#23039=FACE_OUTER_BOUND ( 'NONE', #45294, .T. ) ;
#23080=FACE_OUTER_BOUND ( 'NONE', #96076, .T. ) ;
#23099=ORIENTED_EDGE ( 'NONE', *, *, #90307, .F. ) ;
#23192=DIRECTION ( 'NONE',  ( 0.000000000000000000, 1.000000000000000000, 0.000000000000000000 ) ) ;
#23232=CIRCLE ( 'NONE', #88655, 0.5000000000000004441 ) ;
#23256=DIRECTION ( 'NONE',  ( 0.000000000000000000, 0.000000000000000000, 1.000000000000000000 ) ) ;
#23283=ORIENTED_EDGE ( 'NONE', *, *, #9804, .F. ) ;
#23404=EDGE_CURVE ( 'NONE', #96013, #94251, #95793, .T. ) ;
#23462=DIRECTION ( 'NONE',  ( 0.000000000000000000, 1.000000000000000000, 0.000000000000000000 ) ) ;
#23498=ORIENTED_EDGE ( 'NONE', *, *, #13378, .F. ) ;
#23530=ORIENTED_EDGE ( 'NONE', *, *, #609, .T. ) ;
#23612=AXIS2_PLACEMENT_3D ( 'NONE', #70922, #21345, #96798 ) ;
#23617=DIRECTION ( 'NONE',  ( 0.000000000000000000, 1.000000000000000000, 0.000000000000000000 ) ) ;
#23641=SURFACE_STYLE_USAGE ( .BOTH. , #81300 ) ;
#23645=( LENGTH_UNIT ( ) NAMED_UNIT ( * ) SI_UNIT ( .MILLI., .METRE. ) );
#23690=AXIS2_PLACEMENT_3D ( 'NONE', #96444, #22580, #79180 ) ;
#23695=ORIENTED_EDGE ( 'NONE', *, *, #65236, .F. ) ;
#24061=ORIENTED_EDGE ( 'NONE', *, *, #22604, .T. ) ;
#24134=COLOUR_RGB ( '', 0.08235294, 0.09019608, 0.10196078) ;
#24136=CARTESIAN_POINT ( 'NONE',  ( 1.102182119232617714E-15, -14.49999999999999822, 9.000000000000000000 ) ) ;
#24158=DIRECTION ( 'NONE',  ( 0.000000000000000000, 1.000000000000000000, 0.000000000000000000 ) ) ;
#24167=DIRECTION ( 'NONE',  ( 0.000000000000000000, 0.000000000000000000, 1.000000000000000000 ) ) ;
#24189=DIRECTION ( 'NONE',  ( 0.000000000000000000, 0.000000000000000000, -1.000000000000000000 ) ) ;
#24220=ORIENTED_EDGE ( 'NONE', *, *, #100305, .T. ) ;
#24306=CIRCLE ( 'NONE', #48350, 14.78272384904389192 ) ;
#24418=TOROIDAL_SURFACE ( 'NONE', #29574, 9.000000000000000000, 0.5000000000000000000 ) ;
#24474=TOROIDAL_SURFACE ( 'NONE', #53690, 60.50000000000000000, 0.5000000000000000000 ) ;
#24638=DIRECTION ( 'NONE',  ( 1.000000000000000000, 0.000000000000000000, -1.224646799147353207E-16 ) ) ;
#24705=( NAMED_UNIT ( * ) SI_UNIT ( $, .STERADIAN. ) SOLID_ANGLE_UNIT ( ) );
#24711=FILL_AREA_STYLE_COLOUR ( '', #34778 ) ;
#24753=TOROIDAL_SURFACE ( 'NONE', #90178, 66.00000000000000000, 0.5000000000000000000 ) ;
#24806=EDGE_LOOP ( 'NONE', ( #22229, #51337, #41074, #66163 ) ) ;
#24813=ORIENTED_EDGE ( 'NONE', *, *, #73673, .F. ) ;
#24899=CARTESIAN_POINT ( 'NONE',  ( 0.000000000000000000, 48.50000000000000000, -60.00000000000000000 ) ) ;
#24926=COLOUR_RGB ( '', 0.66274510, 0.83137255, 0.94901961) ;
#25111=( GEOMETRIC_REPRESENTATION_CONTEXT ( 3 ) GLOBAL_UNCERTAINTY_ASSIGNED_CONTEXT ( ( #25736 ) ) GLOBAL_UNIT_ASSIGNED_CONTEXT ( ( #63563, #12853, #96457 ) ) REPRESENTATION_CONTEXT ( 'NONE', 'WORKASPACE' ) );
#25170=DIRECTION ( 'NONE',  ( -1.224646799147349509E-16, 0.000000000000000000, -1.000000000000000000 ) ) ;
#25193=AXIS2_PLACEMENT_3D ( 'NONE', #83847, #51477, #84392 ) ;
#25239=AXIS2_PLACEMENT_3D ( 'NONE', #83380, #9475, #67740 ) ;
#25333=DIRECTION ( 'NONE',  ( 0.000000000000000000, 0.000000000000000000, 1.000000000000000000 ) ) ;
#25340=EDGE_CURVE ( 'NONE', #73687, #80282, #33811, .T. ) ;
#25413=ADVANCED_FACE ( 'NONE', ( #30864 ), #59745, .F. ) ;
#25522=ORIENTED_EDGE ( 'NONE', *, *, #87679, .T. ) ;
#25611=AXIS2_PLACEMENT_3D ( 'NONE', #88017, #95059, #21193 ) ;
#25654=CIRCLE ( 'NONE', #54840, 0.5000000000000004441 ) ;
#25736=UNCERTAINTY_MEASURE_WITH_UNIT (LENGTH_MEASURE( 1.000000000000000082E-05 ), #63563, 'distance_accuracy_value', 'NONE');
#25837=ORIENTED_EDGE ( 'NONE', *, *, #101853, .T. ) ;
#25840=CARTESIAN_POINT ( 'NONE',  ( 0.000000000000000000, 0.000000000000000000, 8.500000000000000000 ) ) ;
#25849=STYLED_ITEM ( 'NONE', ( #96883 ), #34362 ) ;
#25887=DIRECTION ( 'NONE',  ( 0.000000000000000000, 0.000000000000000000, 1.000000000000000000 ) ) ;
#25933=( GEOMETRIC_REPRESENTATION_CONTEXT ( 3 ) GLOBAL_UNCERTAINTY_ASSIGNED_CONTEXT ( ( #103321 ) ) GLOBAL_UNIT_ASSIGNED_CONTEXT ( ( #47253, #97389, #95829 ) ) REPRESENTATION_CONTEXT ( 'NONE', 'WORKASPACE' ) );
#26102=TOROIDAL_SURFACE ( 'NONE', #67413, 64.50000000000000000, 0.5000000000000000000 ) ;
#26111=CARTESIAN_POINT ( 'NONE',  ( 7.592810154713590230E-15, 48.00000000000000000, -62.00000000000000000 ) ) ;
#26115=DIRECTION ( 'NONE',  ( 0.000000000000000000, 0.000000000000000000, 1.000000000000000000 ) ) ;
#26116=EDGE_LOOP ( 'NONE', ( #31281, #73149, #51684, #31159 ) ) ;
#26279=DIRECTION ( 'NONE',  ( 0.000000000000000000, 0.000000000000000000, 1.000000000000000000 ) ) ;
#26283=UNCERTAINTY_MEASURE_WITH_UNIT (LENGTH_MEASURE( 1.000000000000000082E-05 ), #61897, 'distance_accuracy_value', 'NONE');
#26291=DIRECTION ( 'NONE',  ( 0.000000000000000000, 0.000000000000000000, -1.000000000000000000 ) ) ;
#26331=( NAMED_UNIT ( * ) PLANE_ANGLE_UNIT ( ) SI_UNIT ( $, .RADIAN. ) );
#26333=FACE_OUTER_BOUND ( 'NONE', #45742, .T. ) ;
#26352=AXIS2_PLACEMENT_3D ( 'NONE', #41256, #74143, #98941 ) ;
#26362=AXIS2_PLACEMENT_3D ( 'NONE', #38493, #21787, #71354 ) ;
#26373=DIRECTION ( 'NONE',  ( 0.000000000000000000, 1.000000000000000000, 0.000000000000000000 ) ) ;
#26517=DIRECTION ( 'NONE',  ( 0.000000000000000000, 1.000000000000000000, 0.000000000000000000 ) ) ;
#26570=CIRCLE ( 'NONE', #38549, 0.5000000000000004441 ) ;
#26593=ORIENTED_EDGE ( 'NONE', *, *, #64836, .T. ) ;
#26598=DIRECTION ( 'NONE',  ( 0.000000000000000000, 0.000000000000000000, -1.000000000000000000 ) ) ;
#26675=UNCERTAINTY_MEASURE_WITH_UNIT (LENGTH_MEASURE( 1.000000000000000082E-05 ), #58357, 'distance_accuracy_value', 'NONE');
#26684=CARTESIAN_POINT ( 'NONE',  ( 0.000000000000000000, -1.023477375540016387, 0.000000000000000000 ) ) ;
#26734=DIRECTION ( 'NONE',  ( 0.000000000000000000, 0.000000000000000000, 1.000000000000000000 ) ) ;
#26753=AXIS2_PLACEMENT_3D ( 'NONE', #26111, #11449, #9855 ) ;
#26837=DIRECTION ( 'NONE',  ( 0.000000000000000000, 0.000000000000000000, 1.000000000000000000 ) ) ;
#26840=EDGE_LOOP ( 'NONE', ( #76072, #2314, #95349, #11733 ) ) ;
#26851=CIRCLE ( 'NONE', #45746, 60.00000000000000000 ) ;
#26858=SURFACE_STYLE_USAGE ( .BOTH. , #83980 ) ;
#26918=EDGE_LOOP ( 'NONE', ( #13985, #53453, #8213, #42713 ) ) ;
#26942=AXIS2_PLACEMENT_3D ( 'NONE', #21225, #54054, #37937 ) ;
#27081=DIRECTION ( 'NONE',  ( 0.000000000000000000, 0.7310552682428690385, 0.6823182503600110360 ) ) ;
#27118=VECTOR ( 'NONE', #40340, 1000.000000000000114 ) ;
#27243=SURFACE_STYLE_USAGE ( .BOTH. , #103218 ) ;
#27306=CARTESIAN_POINT ( 'NONE',  ( 7.347880794884118356E-15, 0.000000000000000000, -60.00000000000000000 ) ) ;
#27317=CARTESIAN_POINT ( 'NONE',  ( 0.000000000000000000, 80.00000000000000000, -66.00000000000000000 ) ) ;
#27435=CARTESIAN_POINT ( 'NONE',  ( 0.000000000000000000, 0.000000000000000000, 0.000000000000000000 ) ) ;
#27497=ORIENTED_EDGE ( 'NONE', *, *, #44560, .T. ) ;
#27506=SURFACE_STYLE_FILL_AREA ( #68460 ) ;
#27563=CARTESIAN_POINT ( 'NONE',  ( 0.000000000000000000, 79.50000000000000000, 0.000000000000000000 ) ) ;
#27569=SURFACE_STYLE_USAGE ( .BOTH. , #94935 ) ;
#27575=EDGE_LOOP ( 'NONE', ( #36638, #45448, #34595, #84513 ) ) ;
#27728=EDGE_CURVE ( 'NONE', #83020, #75460, #54180, .T. ) ;
#27907=VECTOR ( 'NONE', #71321, 1000.000000000000000 ) ;
#27922=ORIENTED_EDGE ( 'NONE', *, *, #11565, .F. ) ;
#27923=CARTESIAN_POINT ( 'NONE',  ( 1.163414459189985485E-15, 0.000000000000000000, -9.500000000000000000 ) ) ;
#27951=CIRCLE ( 'NONE', #48511, 15.14825148316532832 ) ;
#28019=AXIS2_PLACEMENT_3D ( 'NONE', #41884, #8455, #26291 ) ;
#28073=VERTEX_POINT ( 'NONE', #33832 ) ;
#28094=( NAMED_UNIT ( * ) PLANE_ANGLE_UNIT ( ) SI_UNIT ( $, .RADIAN. ) );
#28213=ORIENTED_EDGE ( 'NONE', *, *, #72104, .T. ) ;
#28265=EDGE_CURVE ( 'NONE', #75460, #77482, #71018, .T. ) ;
#28307=EDGE_LOOP ( 'NONE', ( #77831, #18050, #42200, #50820 ) ) ;
#28405=ORIENTED_EDGE ( 'NONE', *, *, #64836, .F. ) ;
#28445=ADVANCED_FACE ( 'NONE', ( #83913 ), #73686, .T. ) ;
#28512=AXIS2_PLACEMENT_3D ( 'NONE', #102269, #29487, #12188 ) ;
#28582=SURFACE_STYLE_USAGE ( .BOTH. , #78676 ) ;
#28584=MECHANICAL_DESIGN_GEOMETRIC_PRESENTATION_REPRESENTATION('',(#61289),#25111);
#28598=AXIS2_PLACEMENT_3D ( 'NONE', #47985, #80892, #58080 ) ;
#28689=ADVANCED_FACE ( 'NONE', ( #105926 ), #87123, .F. ) ;
#28723=EDGE_CURVE ( 'NONE', #12582, #72821, #92481, .T. ) ;
#28770=EDGE_CURVE ( 'NONE', #43, #21338, #54507, .T. ) ;
#28955=AXIS2_PLACEMENT_3D ( 'NONE', #78615, #4216, #36623 ) ;
#29246=DIRECTION ( 'NONE',  ( 0.000000000000000000, 0.000000000000000000, 1.000000000000000000 ) ) ;
#29324=DIRECTION ( 'NONE',  ( 1.000000000000000000, 0.000000000000000000, -1.224646799147353207E-16 ) ) ;
#29347=AXIS2_PLACEMENT_3D ( 'NONE', #31540, #97292, #48205 ) ;
#29487=DIRECTION ( 'NONE',  ( 0.000000000000000000, 1.000000000000000000, 0.000000000000000000 ) ) ;
#29522=CARTESIAN_POINT ( 'NONE',  ( 0.000000000000000000, 43.00000000000000000, 57.86910460382442523 ) ) ;
#29565=ORIENTED_EDGE ( 'NONE', *, *, #70730, .T. ) ;
#29574=AXIS2_PLACEMENT_3D ( 'NONE', #60969, #62044, #20013 ) ;
#29596=SURFACE_STYLE_FILL_AREA ( #103964 ) ;
#29668=DIRECTION ( 'NONE',  ( 0.000000000000000000, 1.000000000000000000, 0.000000000000000000 ) ) ;
#29710=PRESENTATION_STYLE_ASSIGNMENT (( #61533 ) ) ;
#29804=SURFACE_SIDE_STYLE ('',( #64273 ) ) ;
#29828=ORIENTED_EDGE ( 'NONE', *, *, #106598, .F. ) ;
#29834=CIRCLE ( 'NONE', #9071, 0.5000000000000004441 ) ;
#29848=ADVANCED_FACE ( 'NONE', ( #86748 ), #56429, .F. ) ;
#29881=SURFACE_SIDE_STYLE ('',( #54626 ) ) ;
#29883=FACE_OUTER_BOUND ( 'NONE', #24806, .T. ) ;
#29968=CARTESIAN_POINT ( 'NONE',  ( 0.000000000000000000, 44.84115912518001323, 0.000000000000000000 ) ) ;
#30056=DIRECTION ( 'NONE',  ( 8.355988613032100413E-17, 0.7310552682428690385, -0.6823182503600110360 ) ) ;
#30058=SURFACE_STYLE_USAGE ( .BOTH. , #78570 ) ;
#30111=ADVANCED_FACE ( 'NONE', ( #19127 ), #37566, .T. ) ;
#30142=CYLINDRICAL_SURFACE ( 'NONE', #11748, 65.00000000000000000 ) ;
#30175=CARTESIAN_POINT ( 'NONE',  ( 7.960204194457797252E-15, 0.000000000000000000, -65.00000000000000000 ) ) ;
#30184=CIRCLE ( 'NONE', #73186, 62.00000000000000000 ) ;
#30400=ORIENTED_EDGE ( 'NONE', *, *, #57435, .T. ) ;
#30404=FACE_OUTER_BOUND ( 'NONE', #35679, .T. ) ;
#30407=CARTESIAN_POINT ( 'NONE',  ( 0.000000000000000000, 49.50000000000000000, 0.000000000000000000 ) ) ;
#30425=AXIS2_PLACEMENT_3D ( 'NONE', #54022, #86965, #38417 ) ;
#30495=DIRECTION ( 'NONE',  ( 0.000000000000000000, 1.000000000000000000, 0.000000000000000000 ) ) ;
#30579=CARTESIAN_POINT ( 'NONE',  ( 0.000000000000000000, -14.49999999999999822, 0.000000000000000000 ) ) ;
#30632=( NAMED_UNIT ( * ) SI_UNIT ( $, .STERADIAN. ) SOLID_ANGLE_UNIT ( ) );
#30647=( NAMED_UNIT ( * ) PLANE_ANGLE_UNIT ( ) SI_UNIT ( $, .RADIAN. ) );
#30648=CARTESIAN_POINT ( 'NONE',  ( 0.000000000000000000, -15.00000000000000000, 0.000000000000000000 ) ) ;
#30650=ADVANCED_FACE ( 'NONE', ( #1549 ), #43101, .T. ) ;
#30676=FACE_OUTER_BOUND ( 'NONE', #64186, .T. ) ;
#30824=ORIENTED_EDGE ( 'NONE', *, *, #89055, .T. ) ;
#30864=FACE_OUTER_BOUND ( 'NONE', #1704, .T. ) ;
#30956=VERTEX_POINT ( 'NONE', #48394 ) ;
#31040=DIRECTION ( 'NONE',  ( 0.000000000000000000, 1.000000000000000000, 0.000000000000000000 ) ) ;
#31094=STYLED_ITEM ( 'NONE', ( #13500 ), #80288 ) ;
#31121=SURFACE_STYLE_FILL_AREA ( #87742 ) ;
#31159=ORIENTED_EDGE ( 'NONE', *, *, #13378, .T. ) ;
#31185=ORIENTED_EDGE ( 'NONE', *, *, #2232, .T. ) ;
#31202=CIRCLE ( 'NONE', #32956, 8.000000000000000000 ) ;
#31224=UNCERTAINTY_MEASURE_WITH_UNIT (LENGTH_MEASURE( 1.000000000000000082E-05 ), #21703, 'distance_accuracy_value', 'NONE');
#31239=VERTEX_POINT ( 'NONE', #5770 ) ;
#31277=ORIENTED_EDGE ( 'NONE', *, *, #67180, .F. ) ;
#31281=ORIENTED_EDGE ( 'NONE', *, *, #609, .F. ) ;
#31282=CIRCLE ( 'NONE', #188, 66.00000000000000000 ) ;
#31391=AXIS2_PLACEMENT_3D ( 'NONE', #103701, #29324, #62215 ) ;
#31394=TOROIDAL_SURFACE ( 'NONE', #58939, 57.21727615095610275, 0.5000000000000000000 ) ;
#31410=CIRCLE ( 'NONE', #50306, 0.5000000000000004441 ) ;
#31540=CARTESIAN_POINT ( 'NONE',  ( 0.000000000000000000, -14.49999999999999822, 0.000000000000000000 ) ) ;
#31572=DIRECTION ( 'NONE',  ( 0.000000000000000000, 1.000000000000000000, 0.000000000000000000 ) ) ;
#31609=MECHANICAL_DESIGN_GEOMETRIC_PRESENTATION_REPRESENTATION('',(#74595),#5709);
#31610=ORIENTED_EDGE ( 'NONE', *, *, #89656, .F. ) ;
#31716=ORIENTED_EDGE ( 'NONE', *, *, #91719, .T. ) ;
#31729=CARTESIAN_POINT ( 'NONE',  ( 0.000000000000000000, 48.50000000000000000, 0.000000000000000000 ) ) ;
#31732=AXIS2_PLACEMENT_3D ( 'NONE', #55269, #105432, #88195 ) ;
#31809=AXIS2_PLACEMENT_3D ( 'NONE', #1251, #43348, #2871 ) ;
#31821=AXIS2_PLACEMENT_3D ( 'NONE', #20381, #102836, #12214 ) ;
#31822=DIRECTION ( 'NONE',  ( 0.000000000000000000, 0.000000000000000000, 1.000000000000000000 ) ) ;
#31899=EDGE_CURVE ( 'NONE', #66070, #106756, #5661, .T. ) ;
#31987=ORIENTED_EDGE ( 'NONE', *, *, #38730, .T. ) ;
#32256=CARTESIAN_POINT ( 'NONE',  ( 1.810361544441083977E-15, 0.5000000000000000000, -14.78272384904389192 ) ) ;
#32359=DIRECTION ( 'NONE',  ( -0.000000000000000000, -1.000000000000000000, -0.000000000000000000 ) ) ;
#32403=CIRCLE ( 'NONE', #39248, 8.500000000000000000 ) ;
#32554=DIRECTION ( 'NONE',  ( 0.000000000000000000, 0.000000000000000000, 1.000000000000000000 ) ) ;
#32591=EDGE_CURVE ( 'NONE', #89804, #37408, #84162, .T. ) ;
#32671=AXIS2_PLACEMENT_3D ( 'NONE', #64782, #88006, #38926 ) ;
#32761=ORIENTED_EDGE ( 'NONE', *, *, #46459, .T. ) ;
#32782=DIRECTION ( 'NONE',  ( -0.000000000000000000, -1.000000000000000000, -0.000000000000000000 ) ) ;
#32877=ADVANCED_FACE ( 'NONE', ( #74782 ), #48193, .T. ) ;
#32956=AXIS2_PLACEMENT_3D ( 'NONE', #64488, #13784, #56355 ) ;
#32970=DIRECTION ( 'NONE',  ( 0.000000000000000000, 1.000000000000000000, 0.000000000000000000 ) ) ;
#33103=COLOUR_RGB ( '', 0.72549020, 0.75294118, 0.79215686) ;
#33153=ORIENTED_EDGE ( 'NONE', *, *, #51710, .F. ) ;
#33189=ORIENTED_EDGE ( 'NONE', *, *, #84130, .F. ) ;
#33210=( GEOMETRIC_REPRESENTATION_CONTEXT ( 3 ) GLOBAL_UNCERTAINTY_ASSIGNED_CONTEXT ( ( #6009 ) ) GLOBAL_UNIT_ASSIGNED_CONTEXT ( ( #86345, #46906, #77701 ) ) REPRESENTATION_CONTEXT ( 'NONE', 'WORKASPACE' ) );
#33301=COLOUR_RGB ( '', 0.66274510, 0.83137255, 0.94901961) ;
#33320=CARTESIAN_POINT ( 'NONE',  ( 7.409113134841487507E-15, 49.50000000000000000, -60.50000000000000000 ) ) ;
#33406=ADVANCED_FACE ( 'NONE', ( #100403 ), #85966, .F. ) ;
#33490=VERTEX_POINT ( 'NONE', #51307 ) ;
#33518=CARTESIAN_POINT ( 'NONE',  ( 0.000000000000000000, -1.500000000000000000, 10.00000000000000000 ) ) ;
#33593=STYLED_ITEM ( 'NONE', ( #22567 ), #86480 ) ;
#33665=VECTOR ( 'NONE', #11052, 1000.000000000000000 ) ;
#33668=ORIENTED_EDGE ( 'NONE', *, *, #98962, .F. ) ;
#33729=AXIS2_PLACEMENT_3D ( 'NONE', #104523, #22592, #96974 ) ;
#33736=ADVANCED_FACE ( 'NONE', ( #36125, #21008 ), #70038, .F. ) ;
#33811=CIRCLE ( 'NONE', #47546, 0.5000000000000004441 ) ;
#33832=CARTESIAN_POINT ( 'NONE',  ( 0.000000000000000000, 0.1588408748199928722, 15.14825148316532832 ) ) ;
#34089=DIRECTION ( 'NONE',  ( -0.000000000000000000, -1.000000000000000000, -0.000000000000000000 ) ) ;
#34128=ORIENTED_EDGE ( 'NONE', *, *, #57441, .T. ) ;
#34237=APPLICATION_CONTEXT ( 'automotive_design' ) ;
#34238=DIRECTION ( 'NONE',  ( 0.000000000000000000, 0.000000000000000000, 1.000000000000000000 ) ) ;
#34242=ORIENTED_EDGE ( 'NONE', *, *, #13948, .F. ) ;
#34362=ADVANCED_FACE ( 'NONE', ( #104430 ), #103402, .T. ) ;
#34417=DIRECTION ( 'NONE',  ( -0.000000000000000000, -1.000000000000000000, -0.000000000000000000 ) ) ;
#34431=DIRECTION ( 'NONE',  ( -0.000000000000000000, -1.000000000000000000, -0.000000000000000000 ) ) ;
#34434=FACE_OUTER_BOUND ( 'NONE', #14387, .T. ) ;
#34595=ORIENTED_EDGE ( 'NONE', *, *, #34890, .T. ) ;
#34778=COLOUR_RGB ( '', 0.31764706, 0.68627451, 0.89019608) ;
#34877=DIRECTION ( 'NONE',  ( 0.000000000000000000, 1.000000000000000000, 0.000000000000000000 ) ) ;
#34890=EDGE_CURVE ( 'NONE', #21929, #99989, #8623, .T. ) ;
#34909=DIRECTION ( 'NONE',  ( 0.000000000000000000, 0.000000000000000000, -1.000000000000000000 ) ) ;
#34937=PRESENTATION_STYLE_ASSIGNMENT (( #26858 ) ) ;
#34946=DIRECTION ( 'NONE',  ( 0.000000000000000000, 0.000000000000000000, 1.000000000000000000 ) ) ;
#35218=EDGE_CURVE ( 'NONE', #7894, #59944, #78461, .T. ) ;
#35428=CARTESIAN_POINT ( 'NONE',  ( 0.000000000000000000, 79.50000000000000000, 66.50000000000000000 ) ) ;
#35473=SHAPE_REPRESENTATION_RELATIONSHIP ( 'NONE' , 'NONE' ,  #63931, #56232 ) ;
#35524=CIRCLE ( 'NONE', #52725, 65.50000000000000000 ) ;
#35584=FILL_AREA_STYLE_COLOUR ( '', #19975 ) ;
#35679=EDGE_LOOP ( 'NONE', ( #89925, #20754, #103224, #99682 ) ) ;
#35865=FACE_OUTER_BOUND ( 'NONE', #8846, .T. ) ;
#35869=CIRCLE ( 'NONE', #101270, 61.50000000000000000 ) ;
#35996=AXIS2_PLACEMENT_3D ( 'NONE', #32256, #65670, #72692 ) ;
#36009=DIRECTION ( 'NONE',  ( -0.000000000000000000, -1.000000000000000000, -0.000000000000000000 ) ) ;
#36035=SURFACE_STYLE_USAGE ( .BOTH. , #44088 ) ;
#36072=EDGE_LOOP ( 'NONE', ( #46165, #41327, #85964, #43645 ) ) ;
#36097=VECTOR ( 'NONE', #31040, 1000.000000000000000 ) ;
#36125=FACE_OUTER_BOUND ( 'NONE', #100022, .T. ) ;
#36131=SURFACE_SIDE_STYLE ('',( #27506 ) ) ;
#36258=EDGE_CURVE ( 'NONE', #106756, #77143, #45816, .T. ) ;
#36326=DIRECTION ( 'NONE',  ( 0.000000000000000000, 1.000000000000000000, 0.000000000000000000 ) ) ;
#36333=DIRECTION ( 'NONE',  ( 0.000000000000000000, 0.000000000000000000, -1.000000000000000000 ) ) ;
#36524=AXIS2_PLACEMENT_3D ( 'NONE', #47184, #102380, #88725 ) ;
#36623=DIRECTION ( 'NONE',  ( 0.000000000000000000, 0.000000000000000000, 1.000000000000000000 ) ) ;
#36638=ORIENTED_EDGE ( 'NONE', *, *, #27728, .F. ) ;
#36675=CIRCLE ( 'NONE', #26362, 57.86910460382442523 ) ;
#36700=EDGE_LOOP ( 'NONE', ( #5524, #90282, #51893, #5689 ) ) ;
#36774=DIRECTION ( 'NONE',  ( 0.000000000000000000, 0.000000000000000000, 1.000000000000000000 ) ) ;
#36903=ORIENTED_EDGE ( 'NONE', *, *, #25340, .F. ) ;
#37022=ORIENTED_EDGE ( 'NONE', *, *, #21862, .F. ) ;
#37073=CIRCLE ( 'NONE', #26753, 0.5000000000000004441 ) ;
#37106=EDGE_CURVE ( 'NONE', #50441, #77482, #51099, .T. ) ;
#37169=ORIENTED_EDGE ( 'NONE', *, *, #8993, .T. ) ;
#37184=CARTESIAN_POINT ( 'NONE',  ( 0.000000000000000000, 0.000000000000000000, 0.000000000000000000 ) ) ;
#37193=DIRECTION ( 'NONE',  ( 0.000000000000000000, 0.000000000000000000, 1.000000000000000000 ) ) ;
#37204=DIRECTION ( 'NONE',  ( 0.000000000000000000, 1.000000000000000000, 0.000000000000000000 ) ) ;
#37270=FILL_AREA_STYLE ('',( #62073 ) ) ;
#37297=ORIENTED_EDGE ( 'NONE', *, *, #10539, .T. ) ;
#37370=( LENGTH_UNIT ( ) NAMED_UNIT ( * ) SI_UNIT ( .MILLI., .METRE. ) );
#37408=VERTEX_POINT ( 'NONE', #22664 ) ;
#37456=CARTESIAN_POINT ( 'NONE',  ( 0.000000000000000000, -1.500000000000000000, 0.000000000000000000 ) ) ;
#37488=VERTEX_POINT ( 'NONE', #101312 ) ;
#37497=ORIENTED_EDGE ( 'NONE', *, *, #50118, .T. ) ;
#37566=TOROIDAL_SURFACE ( 'NONE', #78847, 66.00000000000000000, 0.5000000000000000000 ) ;
#37573=CIRCLE ( 'NONE', #1307, 15.43455230191221261 ) ;
#37576=ORIENTED_EDGE ( 'NONE', *, *, #64149, .F. ) ;
#37639=CARTESIAN_POINT ( 'NONE',  ( 0.000000000000000000, -14.49999999999999822, 0.000000000000000000 ) ) ;
#37659=CARTESIAN_POINT ( 'NONE',  ( 0.000000000000000000, 0.000000000000000000, 15.00000000000000000 ) ) ;
#37682=( NAMED_UNIT ( * ) PLANE_ANGLE_UNIT ( ) SI_UNIT ( $, .RADIAN. ) );
#37689=FACE_OUTER_BOUND ( 'NONE', #18846, .T. ) ;
#37736=DIRECTION ( 'NONE',  ( 0.000000000000000000, 1.000000000000000000, 0.000000000000000000 ) ) ;
#37937=DIRECTION ( 'NONE',  ( 0.000000000000000000, -0.000000000000000000, 1.000000000000000000 ) ) ;
#37990=DIRECTION ( 'NONE',  ( -0.000000000000000000, -1.000000000000000000, -0.000000000000000000 ) ) ;
#38041=DIRECTION ( 'NONE',  ( 0.000000000000000000, 0.000000000000000000, 1.000000000000000000 ) ) ;
#38140=CARTESIAN_POINT ( 'NONE',  ( 7.086921372259695358E-15, 43.50000000000000711, -57.86910460382442523 ) ) ;
#38161=ORIENTED_EDGE ( 'NONE', *, *, #61906, .T. ) ;
#38165=AXIS2_PLACEMENT_3D ( 'NONE', #104799, #6626, #95136 ) ;
#38219=VERTEX_POINT ( 'NONE', #51288 ) ;
#38315=DIRECTION ( 'NONE',  ( 0.000000000000000000, 1.000000000000000000, 0.000000000000000000 ) ) ;
#38355=FILL_AREA_STYLE_COLOUR ( '', #19009 ) ;
#38417=DIRECTION ( 'NONE',  ( 0.000000000000000000, 0.000000000000000000, 1.000000000000000000 ) ) ;
#38455=CARTESIAN_POINT ( 'NONE',  ( 8.143901214329899974E-15, 0.000000000000000000, -66.50000000000000000 ) ) ;
#38493=CARTESIAN_POINT ( 'NONE',  ( 0.000000000000000000, 43.50000000000000711, 0.000000000000000000 ) ) ;
#38538=STYLED_ITEM ( 'NONE', ( #68741 ), #21784 ) ;
#38549=AXIS2_PLACEMENT_3D ( 'NONE', #68762, #93012, #72316 ) ;
#38587=CARTESIAN_POINT ( 'NONE',  ( 0.000000000000000000, -14.49999999999999822, 0.000000000000000000 ) ) ;
#38645=ADVANCED_FACE ( 'NONE', ( #2635 ), #104695, .T. ) ;
#38700=( GEOMETRIC_REPRESENTATION_CONTEXT ( 3 ) GLOBAL_UNCERTAINTY_ASSIGNED_CONTEXT ( ( #100917 ) ) GLOBAL_UNIT_ASSIGNED_CONTEXT ( ( #53990, #19574, #94492 ) ) REPRESENTATION_CONTEXT ( 'NONE', 'WORKASPACE' ) );
#38730=EDGE_CURVE ( 'NONE', #21786, #77143, #53215, .T. ) ;
#38749=DIRECTION ( 'NONE',  ( -1.000000000000000000, 0.000000000000000000, 0.000000000000000000 ) ) ;
#38756=DIRECTION ( 'NONE',  ( 0.000000000000000000, 0.000000000000000000, 1.000000000000000000 ) ) ;
#38778=( LENGTH_UNIT ( ) NAMED_UNIT ( * ) SI_UNIT ( .MILLI., .METRE. ) );
#38824=VERTEX_POINT ( 'NONE', #88760 ) ;
#38847=DIRECTION ( 'NONE',  ( 0.000000000000000000, 0.000000000000000000, 1.000000000000000000 ) ) ;
#38926=DIRECTION ( 'NONE',  ( 0.000000000000000000, 0.000000000000000000, 1.000000000000000000 ) ) ;
#38979=FACE_OUTER_BOUND ( 'NONE', #41379, .T. ) ;
#39073=DIRECTION ( 'NONE',  ( 0.000000000000000000, 1.000000000000000000, 0.000000000000000000 ) ) ;
#39248=AXIS2_PLACEMENT_3D ( 'NONE', #30648, #24158, #57004 ) ;
#39262=DIRECTION ( 'NONE',  ( 0.000000000000000000, 0.000000000000000000, 1.000000000000000000 ) ) ;
#39286=DIRECTION ( 'NONE',  ( 0.000000000000000000, 1.000000000000000000, 0.000000000000000000 ) ) ;
#39337=ORIENTED_EDGE ( 'NONE', *, *, #105061, .F. ) ;
#39352=EDGE_CURVE ( 'NONE', #97780, #7894, #75510, .T. ) ;
#39384=SURFACE_STYLE_USAGE ( .BOTH. , #96019 ) ;
#39471=AXIS2_PLACEMENT_3D ( 'NONE', #26684, #18581, #34238 ) ;
#39554=( NAMED_UNIT ( * ) PLANE_ANGLE_UNIT ( ) SI_UNIT ( $, .RADIAN. ) );
#39651=CARTESIAN_POINT ( 'NONE',  ( 0.000000000000000000, 79.50000000000000000, 0.000000000000000000 ) ) ;
#39670=( GEOMETRIC_REPRESENTATION_CONTEXT ( 3 ) GLOBAL_UNCERTAINTY_ASSIGNED_CONTEXT ( ( #98039 ) ) GLOBAL_UNIT_ASSIGNED_CONTEXT ( ( #4210, #37682, #30632 ) ) REPRESENTATION_CONTEXT ( 'NONE', 'WORKASPACE' ) );
#39697=VECTOR ( 'NONE', #99655, 1000.000000000000000 ) ;
#39705=CIRCLE ( 'NONE', #10421, 66.00000000000000000 ) ;
#39816=FILL_AREA_STYLE ('',( #88887 ) ) ;
#40239=EDGE_LOOP ( 'NONE', ( #39337, #1283, #103721, #46133 ) ) ;
#40291=CARTESIAN_POINT ( 'NONE',  ( 0.000000000000000000, -1.500000000000000000, 15.43455230191221261 ) ) ;
#40340=DIRECTION ( 'NONE',  ( 8.355988613032100413E-17, 0.7310552682428690385, -0.6823182503600110360 ) ) ;
#40448=ADVANCED_FACE ( 'NONE', ( #86959 ), #70519, .T. ) ;
#40506=ADVANCED_FACE ( 'NONE', ( #3 ), #74977, .T. ) ;
#40574=AXIS2_PLACEMENT_3D ( 'NONE', #84354, #83804, #92968 ) ;
#40687=ORIENTED_EDGE ( 'NONE', *, *, #50278, .F. ) ;
#40760=UNCERTAINTY_MEASURE_WITH_UNIT (LENGTH_MEASURE( 1.000000000000000082E-05 ), #47275, 'distance_accuracy_value', 'NONE');
#40868=AXIS2_PLACEMENT_3D ( 'NONE', #70778, #103150, #36333 ) ;
#40949=AXIS2_PLACEMENT_3D ( 'NONE', #2095, #93789, #100275 ) ;
#41058=VERTEX_POINT ( 'NONE', #27317 ) ;
#41074=ORIENTED_EDGE ( 'NONE', *, *, #103543, .T. ) ;
#41077=AXIS2_PLACEMENT_3D ( 'NONE', #96000, #56573, #88962 ) ;
#41151=ORIENTED_EDGE ( 'NONE', *, *, #98962, .T. ) ;
#41256=CARTESIAN_POINT ( 'NONE',  ( 0.000000000000000000, 44.00000000000000711, 0.000000000000000000 ) ) ;
#41327=ORIENTED_EDGE ( 'NONE', *, *, #101306, .T. ) ;
#41337=MECHANICAL_DESIGN_GEOMETRIC_PRESENTATION_REPRESENTATION('',(#12082),#39670);
#41353=DIRECTION ( 'NONE',  ( 0.000000000000000000, 1.000000000000000000, 0.000000000000000000 ) ) ;
#41362=MECHANICAL_DESIGN_GEOMETRIC_PRESENTATION_REPRESENTATION('',(#31094),#68942);
#41374=CARTESIAN_POINT ( 'NONE',  ( 0.000000000000000000, 48.50000000000000000, 0.000000000000000000 ) ) ;
#41379=EDGE_LOOP ( 'NONE', ( #59973, #50055, #24813, #48002 ) ) ;
#41417=LINE ( 'NONE', #74310, #39697 ) ;
#41436=DIRECTION ( 'NONE',  ( -1.000000000000000000, 0.000000000000000000, 0.000000000000000000 ) ) ;
#41582=VERTEX_POINT ( 'NONE', #88832 ) ;
#41742=DIRECTION ( 'NONE',  ( 0.000000000000000000, 1.000000000000000000, 0.000000000000000000 ) ) ;
#41868=DIRECTION ( 'NONE',  ( -1.224646799147353454E-16, 0.000000000000000000, -1.000000000000000000 ) ) ;
#41884=CARTESIAN_POINT ( 'NONE',  ( 0.000000000000000000, -14.49999999999999822, 0.000000000000000000 ) ) ;
#41901=CARTESIAN_POINT ( 'NONE',  ( 0.000000000000000000, -1.500000000000000000, 0.000000000000000000 ) ) ;
#41926=DIRECTION ( 'NONE',  ( -0.000000000000000000, -1.000000000000000000, -0.000000000000000000 ) ) ;
#42110=ORIENTED_EDGE ( 'NONE', *, *, #1490, .T. ) ;
#42200=ORIENTED_EDGE ( 'NONE', *, *, #85294, .F. ) ;
#42205=ADVANCED_FACE ( 'NONE', ( #14666 ), #89117, .T. ) ;
#42229=EDGE_CURVE ( 'NONE', #105636, #87282, #35869, .T. ) ;
#42486=DIRECTION ( 'NONE',  ( -1.000000000000000000, 0.000000000000000000, 0.000000000000000000 ) ) ;
#42494=AXIS2_PLACEMENT_3D ( 'NONE', #4571, #39073, #86576 ) ;
#42501=FACE_OUTER_BOUND ( 'NONE', #36072, .T. ) ;
#42713=ORIENTED_EDGE ( 'NONE', *, *, #94792, .F. ) ;
#42801=DIRECTION ( 'NONE',  ( 1.000000000000000000, -0.000000000000000000, 1.224646799147353207E-16 ) ) ;
#42855=CARTESIAN_POINT ( 'NONE',  ( 0.000000000000000000, 0.000000000000000000, 0.000000000000000000 ) ) ;
#42864=ORIENTED_EDGE ( 'NONE', *, *, #50118, .F. ) ;
#42867=AXIS2_PLACEMENT_3D ( 'NONE', #76407, #83441, #18755 ) ;
#42894=AXIS2_PLACEMENT_3D ( 'NONE', #3309, #85288, #91794 ) ;
#42974=ORIENTED_EDGE ( 'NONE', *, *, #94585, .T. ) ;
#43007=PLANE ( 'NONE',  #104675 ) ;
#43024=FACE_OUTER_BOUND ( 'NONE', #3936, .T. ) ;
#43101=CYLINDRICAL_SURFACE ( 'NONE', #72012, 61.50000000000000000 ) ;
#43310=VERTEX_POINT ( 'NONE', #102719 ) ;
#43348=DIRECTION ( 'NONE',  ( 1.000000000000000000, -0.000000000000000000, 1.224646799147353207E-16 ) ) ;
#43363=FACE_OUTER_BOUND ( 'NONE', #74968, .T. ) ;
#43597=DIRECTION ( 'NONE',  ( 0.000000000000000000, 0.000000000000000000, 1.000000000000000000 ) ) ;
#43645=ORIENTED_EDGE ( 'NONE', *, *, #73673, .T. ) ;
#43810=CIRCLE ( 'NONE', #79907, 66.50000000000000000 ) ;
#43819=ORIENTED_EDGE ( 'NONE', *, *, #21411, .F. ) ;
#43823=FILL_AREA_STYLE_COLOUR ( '', #16865 ) ;
#43878=DIRECTION ( 'NONE',  ( -0.000000000000000000, -1.000000000000000000, -0.000000000000000000 ) ) ;
#44050=DIRECTION ( 'NONE',  ( 1.224646799147349509E-16, 0.000000000000000000, -1.000000000000000000 ) ) ;
#44088=SURFACE_SIDE_STYLE ('',( #67304 ) ) ;
#44096=CARTESIAN_POINT ( 'NONE',  ( 0.000000000000000000, 49.50000000000000000, 60.50000000000000000 ) ) ;
#44195=STYLED_ITEM ( 'NONE', ( #80956 ), #25413 ) ;
#44367=CARTESIAN_POINT ( 'NONE',  ( 0.000000000000000000, -2.000000000000000000, 0.000000000000000000 ) ) ;
#44405=CARTESIAN_POINT ( 'NONE',  ( 0.000000000000000000, -1.500000000000000000, 0.000000000000000000 ) ) ;
#44456=EDGE_LOOP ( 'NONE', ( #31185, #64152 ) ) ;
#44474=COLOUR_RGB ( '', 0.08235294, 0.09019608, 0.10196078) ;
#44560=EDGE_CURVE ( 'NONE', #37488, #84910, #18758, .T. ) ;
#44632=DIRECTION ( 'NONE',  ( 0.000000000000000000, 1.000000000000000000, 0.000000000000000000 ) ) ;
#44705=EDGE_LOOP ( 'NONE', ( #70652, #69887 ) ) ;
#44913=UNCERTAINTY_MEASURE_WITH_UNIT (LENGTH_MEASURE( 1.000000000000000082E-05 ), #37370, 'distance_accuracy_value', 'NONE');
#45125=DIRECTION ( 'NONE',  ( 0.000000000000000000, 0.000000000000000000, -1.000000000000000000 ) ) ;
#45132=DIRECTION ( 'NONE',  ( 1.000000000000000000, -0.000000000000000000, 1.224646799147353207E-16 ) ) ;
#45161=( NAMED_UNIT ( * ) SI_UNIT ( $, .STERADIAN. ) SOLID_ANGLE_UNIT ( ) );
#45190=CIRCLE ( 'NONE', #53565, 8.000000000000000000 ) ;
#45278=CARTESIAN_POINT ( 'NONE',  ( 0.000000000000000000, -0.5000000000000000000, 0.000000000000000000 ) ) ;
#45294=EDGE_LOOP ( 'NONE', ( #9176, #95006, #94524, #11215 ) ) ;
#45431=ORIENTED_EDGE ( 'NONE', *, *, #61906, .F. ) ;
#45437=DIRECTION ( 'NONE',  ( -1.000000000000000000, 0.000000000000000000, 0.000000000000000000 ) ) ;
#45448=ORIENTED_EDGE ( 'NONE', *, *, #101853, .F. ) ;
#45494=ORIENTED_EDGE ( 'NONE', *, *, #9834, .F. ) ;
#45526=FILL_AREA_STYLE_COLOUR ( '', #16099 ) ;
#45560=AXIS2_PLACEMENT_3D ( 'NONE', #7560, #63716, #23256 ) ;
#45635=DIRECTION ( 'NONE',  ( 0.000000000000000000, 0.000000000000000000, 1.000000000000000000 ) ) ;
#45680=CARTESIAN_POINT ( 'NONE',  ( 0.000000000000000000, 79.50000000000000000, 0.000000000000000000 ) ) ;
#45726=CIRCLE ( 'NONE', #7747, 15.43455230191221261 ) ;
#45729=SURFACE_STYLE_FILL_AREA ( #103953 ) ;
#45738=CARTESIAN_POINT ( 'NONE',  ( 0.000000000000000000, 45.00000000000000711, -56.99999999999999289 ) ) ;
#45742=EDGE_LOOP ( 'NONE', ( #57353, #98718, #21187, #43819 ) ) ;
#45746=AXIS2_PLACEMENT_3D ( 'NONE', #49222, #97776, #32554 ) ;
#45789=AXIS2_PLACEMENT_3D ( 'NONE', #53786, #21452, #22522 ) ;
#45816=CIRCLE ( 'NONE', #95795, 9.500000000000000000 ) ;
#45861=FACE_OUTER_BOUND ( 'NONE', #82699, .T. ) ;
#45865=ORIENTED_EDGE ( 'NONE', *, *, #94792, .T. ) ;
#46041=( NAMED_UNIT ( * ) SI_UNIT ( $, .STERADIAN. ) SOLID_ANGLE_UNIT ( ) );
#46057=TOROIDAL_SURFACE ( 'NONE', #8147, 66.00000000000000000, 0.5000000000000000000 ) ;
#46133=ORIENTED_EDGE ( 'NONE', *, *, #28770, .F. ) ;
#46165=ORIENTED_EDGE ( 'NONE', *, *, #35218, .F. ) ;
#46250=ADVANCED_FACE ( 'NONE', ( #94288 ), #82684, .T. ) ;
#46305=LINE ( 'NONE', #62492, #21655 ) ;
#46330=EDGE_CURVE ( 'NONE', #73621, #8869, #53445, .T. ) ;
#46332=EDGE_CURVE ( 'NONE', #77482, #50441, #87858, .T. ) ;
#46443=AXIS2_PLACEMENT_3D ( 'NONE', #94867, #5314, #85712 ) ;
#46459=EDGE_CURVE ( 'NONE', #37408, #22823, #86257, .T. ) ;
#46473=DIRECTION ( 'NONE',  ( 0.000000000000000000, 0.000000000000000000, 1.000000000000000000 ) ) ;
#46498=FACE_OUTER_BOUND ( 'NONE', #7780, .T. ) ;
#46522=TOROIDAL_SURFACE ( 'NONE', #67251, 62.00000000000000000, 0.5000000000000000000 ) ;
#46573=ORIENTED_EDGE ( 'NONE', *, *, #42229, .F. ) ;
#46679=CIRCLE ( 'NONE', #133, 57.86910460382442523 ) ;
#46793=CARTESIAN_POINT ( 'NONE',  ( 1.832743656797419977E-15, 0.000000000000000000, -14.78272384904389192 ) ) ;
#46838=COLOUR_RGB ( '', 0.31764706, 0.68627451, 0.89019608) ;
#46867=CYLINDRICAL_SURFACE ( 'NONE', #72746, 66.50000000000000000 ) ;
#46873=DIRECTION ( 'NONE',  ( 1.224646799147349509E-16, 0.000000000000000000, -1.000000000000000000 ) ) ;
#46906=( NAMED_UNIT ( * ) PLANE_ANGLE_UNIT ( ) SI_UNIT ( $, .RADIAN. ) );
#46959=AXIS2_PLACEMENT_3D ( 'NONE', #74360, #23192, #6974 ) ;
#47063=SURFACE_STYLE_USAGE ( .BOTH. , #63811 ) ;
#47082=CARTESIAN_POINT ( 'NONE',  ( 7.960204194457797252E-15, 79.50000000000000000, -65.00000000000000000 ) ) ;
#47164=FACE_OUTER_BOUND ( 'NONE', #13359, .T. ) ;
#47184=CARTESIAN_POINT ( 'NONE',  ( 1.040949779275250140E-15, -0.5000000000000000000, -8.500000000000000000 ) ) ;
#47253=( LENGTH_UNIT ( ) NAMED_UNIT ( * ) SI_UNIT ( .MILLI., .METRE. ) );
#47275=( LENGTH_UNIT ( ) NAMED_UNIT ( * ) SI_UNIT ( .MILLI., .METRE. ) );
#47412=CIRCLE ( 'NONE', #885, 0.5000000000000004441 ) ;
#47546=AXIS2_PLACEMENT_3D ( 'NONE', #92902, #45437, #84823 ) ;
#47598=AXIS2_PLACEMENT_3D ( 'NONE', #44405, #2862, #61123 ) ;
#47635=AXIS2_PLACEMENT_3D ( 'NONE', #75569, #67491, #51815 ) ;
#47857=EDGE_CURVE ( 'NONE', #41582, #89804, #31282, .T. ) ;
#47866=TOROIDAL_SURFACE ( 'NONE', #104692, 10.00000000000000000, 0.5000000000000000000 ) ;
#47878=DIRECTION ( 'NONE',  ( 1.000000000000000000, 0.000000000000000000, 0.000000000000000000 ) ) ;
#47985=CARTESIAN_POINT ( 'NONE',  ( 7.898971854500428100E-15, 50.50000000000000000, -64.50000000000000000 ) ) ;
#48002=ORIENTED_EDGE ( 'NONE', *, *, #58110, .F. ) ;
#48099=DIRECTION ( 'NONE',  ( 0.000000000000000000, 1.000000000000000000, 0.000000000000000000 ) ) ;
#48193=TOROIDAL_SURFACE ( 'NONE', #20711, 66.00000000000000000, 0.5000000000000000000 ) ;
#48205=DIRECTION ( 'NONE',  ( 0.000000000000000000, 0.000000000000000000, -1.000000000000000000 ) ) ;
#48214=ORIENTED_EDGE ( 'NONE', *, *, #27728, .T. ) ;
#48306=AXIS2_PLACEMENT_3D ( 'NONE', #20662, #53501, #78296 ) ;
#48350=AXIS2_PLACEMENT_3D ( 'NONE', #51047, #99607, #26837 ) ;
#48380=( NAMED_UNIT ( * ) SI_UNIT ( $, .STERADIAN. ) SOLID_ANGLE_UNIT ( ) );
#48394=CARTESIAN_POINT ( 'NONE',  ( 7.500961644777538868E-15, 43.50000000000000711, -61.00000000000000000 ) ) ;
#48441=EDGE_LOOP ( 'NONE', ( #98723, #52009, #6833, #33668 ) ) ;
#48511=AXIS2_PLACEMENT_3D ( 'NONE', #49706, #91256, #17366 ) ;
#48609=CIRCLE ( 'NONE', #17626, 57.21727615095610275 ) ;
#48707=ADVANCED_FACE ( 'NONE', ( #10692, #37689 ), #20984, .T. ) ;
#48717=COLOUR_RGB ( '', 0.09019608, 0.27058824, 0.51372549) ;
#48808=LINE ( 'NONE', #104954, #4136 ) ;
#48888=DIRECTION ( 'NONE',  ( -0.000000000000000000, -1.000000000000000000, -0.000000000000000000 ) ) ;
#48931=CIRCLE ( 'NONE', #66197, 8.500000000000000000 ) ;
#49107=DIRECTION ( 'NONE',  ( 0.000000000000000000, 0.000000000000000000, -1.000000000000000000 ) ) ;
#49114=CARTESIAN_POINT ( 'NONE',  ( 0.000000000000000000, -1.500000000000000000, 0.000000000000000000 ) ) ;
#49169=EDGE_LOOP ( 'NONE', ( #31277, #60723, #11339, #14834 ) ) ;
#49222=CARTESIAN_POINT ( 'NONE',  ( 0.000000000000000000, 45.50000000000000711, 0.000000000000000000 ) ) ;
#49230=PRODUCT_CONTEXT ( 'NONE', #54819, 'mechanical' ) ;
#49283=CARTESIAN_POINT ( 'NONE',  ( 0.000000000000000000, 50.50000000000000000, 65.00000000000000000 ) ) ;
#49487=LINE ( 'NONE', #65681, #27118 ) ;
#49625=CARTESIAN_POINT ( 'NONE',  ( 1.912569619637256418E-15, -1.500000000000000000, -15.43455230191221261 ) ) ;
#49706=CARTESIAN_POINT ( 'NONE',  ( 0.000000000000000000, 0.1588408748199928722, 0.000000000000000000 ) ) ;
#49785=CIRCLE ( 'NONE', #11911, 15.80007993603364724 ) ;
#49983=CARTESIAN_POINT ( 'NONE',  ( 0.000000000000000000, 79.50000000000000000, 0.000000000000000000 ) ) ;
#50012=EDGE_CURVE ( 'NONE', #8869, #73621, #24306, .T. ) ;
#50033=PRESENTATION_STYLE_ASSIGNMENT (( #36035 ) ) ;
#50055=ORIENTED_EDGE ( 'NONE', *, *, #21526, .T. ) ;
#50118=EDGE_CURVE ( 'NONE', #43310, #6068, #82789, .T. ) ;
#50213=DIRECTION ( 'NONE',  ( 0.000000000000000000, 0.000000000000000000, 1.000000000000000000 ) ) ;
#50253=CARTESIAN_POINT ( 'NONE',  ( 0.000000000000000000, 79.50000000000000000, -66.00000000000000000 ) ) ;
#50278=EDGE_CURVE ( 'NONE', #38824, #74088, #46679, .T. ) ;
#50306=AXIS2_PLACEMENT_3D ( 'NONE', #8565, #67875, #43597 ) ;
#50441=VERTEX_POINT ( 'NONE', #6216 ) ;
#50471=ORIENTED_EDGE ( 'NONE', *, *, #23404, .T. ) ;
#50513=AXIS2_PLACEMENT_3D ( 'NONE', #33320, #7410, #106102 ) ;
#50627=ORIENTED_EDGE ( 'NONE', *, *, #36258, .T. ) ;
#50726=ADVANCED_FACE ( 'NONE', ( #29883 ), #71897, .F. ) ;
#50770=DIRECTION ( 'NONE',  ( 0.000000000000000000, 0.000000000000000000, 1.000000000000000000 ) ) ;
#50820=ORIENTED_EDGE ( 'NONE', *, *, #93977, .F. ) ;
#50844=FILL_AREA_STYLE ('',( #92911 ) ) ;
#50874=ORIENTED_EDGE ( 'NONE', *, *, #67008, .F. ) ;
#51008=CARTESIAN_POINT ( 'NONE',  ( 0.000000000000000000, 50.00000000000000000, 0.000000000000000000 ) ) ;
#51030=ORIENTED_EDGE ( 'NONE', *, *, #20025, .T. ) ;
#51047=CARTESIAN_POINT ( 'NONE',  ( 0.000000000000000000, 0.000000000000000000, 0.000000000000000000 ) ) ;
#51055=VECTOR ( 'NONE', #30056, 1000.000000000000114 ) ;
#51099=CIRCLE ( 'NONE', #97521, 57.50357696970299770 ) ;
#51230=DIRECTION ( 'NONE',  ( 0.000000000000000000, 1.000000000000000000, 0.000000000000000000 ) ) ;
#51288=CARTESIAN_POINT ( 'NONE',  ( 0.000000000000000000, 49.50000000000000000, 60.00000000000000000 ) ) ;
#51307=CARTESIAN_POINT ( 'NONE',  ( 0.000000000000000000, 43.50000000000000711, 61.00000000000000000 ) ) ;
#51337=ORIENTED_EDGE ( 'NONE', *, *, #11628, .T. ) ;
#51383=SURFACE_STYLE_FILL_AREA ( #50844 ) ;
#51398=EDGE_CURVE ( 'NONE', #61967, #91723, #22756, .T. ) ;
#51436=UNCERTAINTY_MEASURE_WITH_UNIT (LENGTH_MEASURE( 1.000000000000000082E-05 ), #19688, 'distance_accuracy_value', 'NONE');
#51477=DIRECTION ( 'NONE',  ( 0.000000000000000000, 1.000000000000000000, 0.000000000000000000 ) ) ;
#51483=COLOUR_RGB ( '', 0.72549020, 0.75294118, 0.79215686) ;
#51585=ORIENTED_EDGE ( 'NONE', *, *, #37106, .T. ) ;
#51684=ORIENTED_EDGE ( 'NONE', *, *, #80730, .T. ) ;
#51685=DIRECTION ( 'NONE',  ( 0.000000000000000000, 1.000000000000000000, 0.000000000000000000 ) ) ;
#51710=EDGE_CURVE ( 'NONE', #33490, #30956, #71004, .T. ) ;
#51766=PRODUCT_DEFINITION_SHAPE ( 'NONE', 'NONE',  #73291 ) ;
#51795=ADVANCED_FACE ( 'NONE', ( #104035 ), #46867, .T. ) ;
#51815=DIRECTION ( 'NONE',  ( 0.000000000000000000, 0.000000000000000000, 1.000000000000000000 ) ) ;
#51829=EDGE_CURVE ( 'NONE', #94251, #21876, #79236, .T. ) ;
#51893=ORIENTED_EDGE ( 'NONE', *, *, #106598, .T. ) ;
#52009=ORIENTED_EDGE ( 'NONE', *, *, #89656, .T. ) ;
#52058=CIRCLE ( 'NONE', #28019, 9.500000000000000000 ) ;
#52092=PRODUCT_DEFINITION_CONTEXT ( 'detailed design', #34237, 'design' ) ;
#52158=FACE_OUTER_BOUND ( 'NONE', #26840, .T. ) ;
#52195=TOROIDAL_SURFACE ( 'NONE', #57425, 8.500000000000000000, 0.5000000000000000000 ) ;
#52216=DIRECTION ( 'NONE',  ( 0.000000000000000000, 0.000000000000000000, 1.000000000000000000 ) ) ;
#52241=DIRECTION ( 'NONE',  ( 0.000000000000000000, 1.000000000000000000, 0.000000000000000000 ) ) ;
#52284=( GEOMETRIC_REPRESENTATION_CONTEXT ( 3 ) GLOBAL_UNCERTAINTY_ASSIGNED_CONTEXT ( ( #51436 ) ) GLOBAL_UNIT_ASSIGNED_CONTEXT ( ( #19688, #39554, #72430 ) ) REPRESENTATION_CONTEXT ( 'NONE', 'WORKASPACE' ) );
#52317=FILL_AREA_STYLE ('',( #78194 ) ) ;
#52429=ADVANCED_FACE ( 'NONE', ( #99939 ), #12548, .F. ) ;
#52446=AXIS2_PLACEMENT_3D ( 'NONE', #61597, #103623, #86411 ) ;
#52725=AXIS2_PLACEMENT_3D ( 'NONE', #16809, #34089, #66961 ) ;
#52770=AXIS2_PLACEMENT_3D ( 'NONE', #9890, #42801, #7766 ) ;
#52949=PRESENTATION_STYLE_ASSIGNMENT (( #11948 ) ) ;
#52989=SURFACE_SIDE_STYLE ('',( #69188 ) ) ;
#53215=LINE ( 'NONE', #27923, #82284 ) ;
#53257=ORIENTED_EDGE ( 'NONE', *, *, #8993, .F. ) ;
#53332=CARTESIAN_POINT ( 'NONE',  ( 0.000000000000000000, 44.84115912518001323, 56.85174851683467523 ) ) ;
#53393=CIRCLE ( 'NONE', #56835, 65.00000000000000000 ) ;
#53405=EDGE_LOOP ( 'NONE', ( #15179, #98926, #69580, #50627 ) ) ;
#53445=CIRCLE ( 'NONE', #98156, 14.78272384904389192 ) ;
#53453=ORIENTED_EDGE ( 'NONE', *, *, #10689, .T. ) ;
#53501=DIRECTION ( 'NONE',  ( -1.000000000000000000, 0.000000000000000000, 0.000000000000000000 ) ) ;
#53565=AXIS2_PLACEMENT_3D ( 'NONE', #74985, #1076, #77677 ) ;
#53582=ORIENTED_EDGE ( 'NONE', *, *, #22604, .F. ) ;
#53583=ADVANCED_FACE ( 'NONE', ( #45861 ), #86661, .F. ) ;
#53589=ORIENTED_EDGE ( 'NONE', *, *, #76103, .T. ) ;
#53690=AXIS2_PLACEMENT_3D ( 'NONE', #15212, #48099, #70281 ) ;
#53694=ORIENTED_EDGE ( 'NONE', *, *, #105400, .F. ) ;
#53761=FACE_OUTER_BOUND ( 'NONE', #58432, .T. ) ;
#53786=CARTESIAN_POINT ( 'NONE',  ( 0.000000000000000000, -1.023477375540016387, 0.000000000000000000 ) ) ;
#53800=EDGE_CURVE ( 'NONE', #14939, #84383, #29834, .T. ) ;
#53817=DIRECTION ( 'NONE',  ( 0.000000000000000000, 1.000000000000000000, 0.000000000000000000 ) ) ;
#53947=EDGE_CURVE ( 'NONE', #62139, #97780, #96938, .T. ) ;
#53990=( LENGTH_UNIT ( ) NAMED_UNIT ( * ) SI_UNIT ( .MILLI., .METRE. ) );
#54015=VERTEX_POINT ( 'NONE', #12291 ) ;
#54021=CARTESIAN_POINT ( 'NONE',  ( 7.347880794884118356E-15, 45.50000000000000711, -60.00000000000000000 ) ) ;
#54022=CARTESIAN_POINT ( 'NONE',  ( 0.000000000000000000, 43.00000000000000000, 0.000000000000000000 ) ) ;
#54054=DIRECTION ( 'NONE',  ( 0.000000000000000000, 1.000000000000000000, 0.000000000000000000 ) ) ;
#54180=CIRCLE ( 'NONE', #31809, 0.4999999999999987232 ) ;
#54185=DIRECTION ( 'NONE',  ( 0.000000000000000000, 0.000000000000000000, 1.000000000000000000 ) ) ;
#54328=AXIS2_PLACEMENT_3D ( 'NONE', #21495, #23617, #39262 ) ;
#54355=AXIS2_PLACEMENT_3D ( 'NONE', #56847, #105929, #6172 ) ;
#54384=AXIS2_PLACEMENT_3D ( 'NONE', #45278, #37204, #5345 ) ;
#54477=SURFACE_STYLE_USAGE ( .BOTH. , #97081 ) ;
#54507=CIRCLE ( 'NONE', #8096, 0.5000000000000004441 ) ;
#54538=SURFACE_STYLE_FILL_AREA ( #6003 ) ;
#54546=UNCERTAINTY_MEASURE_WITH_UNIT (LENGTH_MEASURE( 1.000000000000000082E-05 ), #1217, 'distance_accuracy_value', 'NONE');
#54582=EDGE_LOOP ( 'NONE', ( #27922, #50471, #90561, #29828 ) ) ;
#54626=SURFACE_STYLE_FILL_AREA ( #20757 ) ;
#54651=DIRECTION ( 'NONE',  ( 0.000000000000000000, 1.000000000000000000, 0.000000000000000000 ) ) ;
#54774=VECTOR ( 'NONE', #38315, 1000.000000000000000 ) ;
#54819=APPLICATION_CONTEXT ( 'automotive_design' ) ;
#54840=AXIS2_PLACEMENT_3D ( 'NONE', #24136, #100106, #41868 ) ;
#54986=SURFACE_SIDE_STYLE ('',( #78735 ) ) ;
#55162=DIRECTION ( 'NONE',  ( 1.224646799147353454E-16, 0.000000000000000000, -1.000000000000000000 ) ) ;
#55269=CARTESIAN_POINT ( 'NONE',  ( 0.000000000000000000, 44.00000000000000711, 61.00000000000000000 ) ) ;
#55378=DIRECTION ( 'NONE',  ( 0.000000000000000000, 0.000000000000000000, -1.000000000000000000 ) ) ;
#55430=ADVANCED_FACE ( 'NONE', ( #92229 ), #88544, .T. ) ;
#55443=AXIS2_PLACEMENT_3D ( 'NONE', #97851, #41742, #67093 ) ;
#55518=FILL_AREA_STYLE_COLOUR ( '', #44474 ) ;
#55528=( GEOMETRIC_REPRESENTATION_CONTEXT ( 3 ) GLOBAL_UNCERTAINTY_ASSIGNED_CONTEXT ( ( #91714 ) ) GLOBAL_UNIT_ASSIGNED_CONTEXT ( ( #85601, #26331, #2523 ) ) REPRESENTATION_CONTEXT ( 'NONE', 'WORKASPACE' ) );
#55575=CYLINDRICAL_SURFACE ( 'NONE', #45560, 60.00000000000000000 ) ;
#55577=DIRECTION ( 'NONE',  ( 0.000000000000000000, 0.000000000000000000, 1.000000000000000000 ) ) ;
#55580=EDGE_LOOP ( 'NONE', ( #5717, #25522, #23498, #28405 ) ) ;
#55638=FACE_OUTER_BOUND ( 'NONE', #44705, .T. ) ;
#55649=DIRECTION ( 'NONE',  ( 0.000000000000000000, 0.000000000000000000, 1.000000000000000000 ) ) ;
#55761=ORIENTED_EDGE ( 'NONE', *, *, #56973, .T. ) ;
#55799=CARTESIAN_POINT ( 'NONE',  ( 0.000000000000000000, 44.00000000000000711, 61.50000000000000000 ) ) ;
#55861=PRESENTATION_STYLE_ASSIGNMENT (( #30058 ) ) ;
#55950=PRESENTATION_STYLE_ASSIGNMENT (( #60905 ) ) ;
#56064=CARTESIAN_POINT ( 'NONE',  ( 9.797174393178825657E-16, -14.49999999999999822, -8.000000000000000000 ) ) ;
#56232=ADVANCED_BREP_SHAPE_REPRESENTATION ( '', ( #89707, #10728 ), #79579 ) ;
#56344=CARTESIAN_POINT ( 'NONE',  ( 7.007095409419855762E-15, 45.00000000000000711, -57.21727615095610275 ) ) ;
#56355=DIRECTION ( 'NONE',  ( 0.000000000000000000, 0.000000000000000000, 1.000000000000000000 ) ) ;
#56377=CIRCLE ( 'NONE', #9888, 59.50000000000000000 ) ;
#56429=CONICAL_SURFACE ( 'NONE', #28955, 15.00000000000000000, 0.7509290623979402168 ) ;
#56451=DIRECTION ( 'NONE',  ( 0.000000000000000000, 0.000000000000000000, 1.000000000000000000 ) ) ;
#56534=ORIENTED_EDGE ( 'NONE', *, *, #92919, .T. ) ;
#56573=DIRECTION ( 'NONE',  ( 0.000000000000000000, 1.000000000000000000, 0.000000000000000000 ) ) ;
#56835=AXIS2_PLACEMENT_3D ( 'NONE', #70428, #80087, #5160 ) ;
#56847=CARTESIAN_POINT ( 'NONE',  ( 0.000000000000000000, 0.000000000000000000, 0.000000000000000000 ) ) ;
#56857=DIRECTION ( 'NONE',  ( 0.000000000000000000, 0.000000000000000000, -1.000000000000000000 ) ) ;
#56973=EDGE_CURVE ( 'NONE', #22823, #37408, #88849, .T. ) ;
#57004=DIRECTION ( 'NONE',  ( 0.000000000000000000, 0.000000000000000000, -1.000000000000000000 ) ) ;
#57012=DIRECTION ( 'NONE',  ( 0.000000000000000000, 0.000000000000000000, 1.000000000000000000 ) ) ;
#57033=DIRECTION ( 'NONE',  ( 0.000000000000000000, 0.000000000000000000, 1.000000000000000000 ) ) ;
#57035=SURFACE_SIDE_STYLE ('',( #18214 ) ) ;
#57124=CARTESIAN_POINT ( 'NONE',  ( 0.000000000000000000, -0.5000000000000000000, 0.000000000000000000 ) ) ;
#57159=DIRECTION ( 'NONE',  ( -1.000000000000000000, 0.000000000000000000, 0.000000000000000000 ) ) ;
#57272=( NAMED_UNIT ( * ) PLANE_ANGLE_UNIT ( ) SI_UNIT ( $, .RADIAN. ) );
#57310=CIRCLE ( 'NONE', #26352, 61.50000000000000000 ) ;
#57337=STYLED_ITEM ( 'NONE', ( #29710 ), #53583 ) ;
#57353=ORIENTED_EDGE ( 'NONE', *, *, #20430, .F. ) ;
#57401=ORIENTED_EDGE ( 'NONE', *, *, #105061, .T. ) ;
#57425=AXIS2_PLACEMENT_3D ( 'NONE', #37639, #96893, #71536 ) ;
#57435=EDGE_CURVE ( 'NONE', #84910, #84383, #1115, .T. ) ;
#57441=EDGE_CURVE ( 'NONE', #6068, #43310, #35524, .T. ) ;
#57514=CARTESIAN_POINT ( 'NONE',  ( 0.000000000000000000, 43.34115912517999902, 0.000000000000000000 ) ) ;
#57555=ORIENTED_EDGE ( 'NONE', *, *, #94585, .F. ) ;
#57577=EDGE_CURVE ( 'NONE', #94251, #92669, #97520, .T. ) ;
#57662=ORIENTED_EDGE ( 'NONE', *, *, #93514, .T. ) ;
#57860=TOROIDAL_SURFACE ( 'NONE', #54384, 8.500000000000000000, 0.5000000000000000000 ) ;
#58080=DIRECTION ( 'NONE',  ( 1.224646799147349509E-16, 0.000000000000000000, -1.000000000000000000 ) ) ;
#58110=EDGE_CURVE ( 'NONE', #61967, #38219, #80429, .T. ) ;
#58277=CARTESIAN_POINT ( 'NONE',  ( 0.000000000000000000, -1.341159125180006795, 0.000000000000000000 ) ) ;
#58357=( LENGTH_UNIT ( ) NAMED_UNIT ( * ) SI_UNIT ( .MILLI., .METRE. ) );
#58376=ORIENTED_EDGE ( 'NONE', *, *, #64149, .T. ) ;
#58426=MECHANICAL_DESIGN_GEOMETRIC_PRESENTATION_REPRESENTATION('',(#89460),#79126);
#58432=EDGE_LOOP ( 'NONE', ( #65949, #7065, #72125, #84895 ) ) ;
#58892=CARTESIAN_POINT ( 'NONE',  ( 0.000000000000000000, 50.00000000000000000, 60.50000000000000000 ) ) ;
#58939=AXIS2_PLACEMENT_3D ( 'NONE', #78560, #64518, #104976 ) ;
#59080=ADVANCED_FACE ( 'NONE', ( #4970 ), #47866, .F. ) ;
#59186=CARTESIAN_POINT ( 'NONE',  ( 7.592810154713590230E-15, 48.50000000000000000, -62.00000000000000000 ) ) ;
#59188=CARTESIAN_POINT ( 'NONE',  ( 0.000000000000000000, 48.50000000000000000, 66.00000000000000000 ) ) ;
#59237=CYLINDRICAL_SURFACE ( 'NONE', #13373, 60.00000000000000000 ) ;
#59269=ADVANCED_FACE ( 'NONE', ( #42501 ), #59237, .F. ) ;
#59272=ORIENTED_EDGE ( 'NONE', *, *, #39352, .T. ) ;
#59276=EDGE_LOOP ( 'NONE', ( #8192, #79230 ) ) ;
#59430=CARTESIAN_POINT ( 'NONE',  ( 7.960204194457797252E-15, 50.50000000000000000, -65.00000000000000000 ) ) ;
#59456=CIRCLE ( 'NONE', #93854, 60.00000000000000000 ) ;
#59533=ORIENTED_EDGE ( 'NONE', *, *, #98033, .T. ) ;
#59745=TOROIDAL_SURFACE ( 'NONE', #30425, 57.86910460382442523, 0.5000000000000000000 ) ;
#59829=CARTESIAN_POINT ( 'NONE',  ( 0.000000000000000000, 0.000000000000000000, 0.000000000000000000 ) ) ;
#59846=ADVANCED_FACE ( 'NONE', ( #46498, #78856 ), #93992, .T. ) ;
#59881=CIRCLE ( 'NONE', #8194, 8.000000000000000000 ) ;
#59944=VERTEX_POINT ( 'NONE', #11996 ) ;
#59973=ORIENTED_EDGE ( 'NONE', *, *, #63726, .F. ) ;
#60079=EDGE_LOOP ( 'NONE', ( #73056, #74864, #95390, #106631 ) ) ;
#60098=ORIENTED_EDGE ( 'NONE', *, *, #93246, .F. ) ;
#60150=AXIS2_PLACEMENT_3D ( 'NONE', #2538, #1998, #34946 ) ;
#60249=VERTEX_POINT ( 'NONE', #33518 ) ;
#60276=( NAMED_UNIT ( * ) SI_UNIT ( $, .STERADIAN. ) SOLID_ANGLE_UNIT ( ) );
#60296=CARTESIAN_POINT ( 'NONE',  ( 0.000000000000000000, 0.000000000000000000, 0.000000000000000000 ) ) ;
#60312=AXIS2_PLACEMENT_3D ( 'NONE', #103433, #95883, #22007 ) ;
#60450=( NAMED_UNIT ( * ) SI_UNIT ( $, .STERADIAN. ) SOLID_ANGLE_UNIT ( ) );
#60569=PRESENTATION_STYLE_ASSIGNMENT (( #101539 ) ) ;
#60627=DIRECTION ( 'NONE',  ( 0.000000000000000000, 0.000000000000000000, -1.000000000000000000 ) ) ;
#60655=( GEOMETRIC_REPRESENTATION_CONTEXT ( 3 ) GLOBAL_UNCERTAINTY_ASSIGNED_CONTEXT ( ( #91493 ) ) GLOBAL_UNIT_ASSIGNED_CONTEXT ( ( #99651, #18231, #45161 ) ) REPRESENTATION_CONTEXT ( 'NONE', 'WORKASPACE' ) );
#60723=ORIENTED_EDGE ( 'NONE', *, *, #94232, .T. ) ;
#60905=SURFACE_STYLE_USAGE ( .BOTH. , #36131 ) ;
#60969=CARTESIAN_POINT ( 'NONE',  ( 0.000000000000000000, -14.49999999999999822, 0.000000000000000000 ) ) ;
#61123=DIRECTION ( 'NONE',  ( 0.000000000000000000, 0.000000000000000000, 1.000000000000000000 ) ) ;
#61200=AXIS2_PLACEMENT_3D ( 'NONE', #45680, #61882, #103896 ) ;
#61289=STYLED_ITEM ( 'NONE', ( #55950 ), #63551 ) ;
#61344=DIRECTION ( 'NONE',  ( 0.000000000000000000, 0.000000000000000000, 1.000000000000000000 ) ) ;
#61533=SURFACE_STYLE_USAGE ( .BOTH. , #54986 ) ;
#61597=CARTESIAN_POINT ( 'NONE',  ( 0.000000000000000000, 48.00000000000000000, 0.000000000000000000 ) ) ;
#61646=AXIS2_PLACEMENT_3D ( 'NONE', #24899, #26517, #66941 ) ;
#61688=EDGE_LOOP ( 'NONE', ( #87922, #40687, #5148, #75201 ) ) ;
#61834=DIRECTION ( 'NONE',  ( -0.000000000000000000, -1.000000000000000000, -0.000000000000000000 ) ) ;
#61853=EDGE_CURVE ( 'NONE', #37488, #73687, #48931, .T. ) ;
#61882=DIRECTION ( 'NONE',  ( 0.000000000000000000, 1.000000000000000000, 0.000000000000000000 ) ) ;
#61897=( LENGTH_UNIT ( ) NAMED_UNIT ( * ) SI_UNIT ( .MILLI., .METRE. ) );
#61906=EDGE_CURVE ( 'NONE', #33490, #2579, #102390, .T. ) ;
#61917=AXIS2_PLACEMENT_3D ( 'NONE', #66916, #32970, #15688 ) ;
#61921=DIRECTION ( 'NONE',  ( 0.000000000000000000, 0.7310552682428690385, 0.6823182503600110360 ) ) ;
#61967=VERTEX_POINT ( 'NONE', #58892 ) ;
#61996=DIRECTION ( 'NONE',  ( 0.000000000000000000, 0.000000000000000000, -1.000000000000000000 ) ) ;
#62044=DIRECTION ( 'NONE',  ( -0.000000000000000000, -1.000000000000000000, -0.000000000000000000 ) ) ;
#62073=FILL_AREA_STYLE_COLOUR ( '', #48717 ) ;
#62139=VERTEX_POINT ( 'NONE', #67510 ) ;
#62215=DIRECTION ( 'NONE',  ( -1.224646799147349509E-16, 0.000000000000000000, -1.000000000000000000 ) ) ;
#62279=DIRECTION ( 'NONE',  ( -1.000000000000000000, 0.000000000000000000, 0.000000000000000000 ) ) ;
#62334=CIRCLE ( 'NONE', #88192, 56.85174851683467523 ) ;
#62474=ORIENTED_EDGE ( 'NONE', *, *, #51829, .F. ) ;
#62492=CARTESIAN_POINT ( 'NONE',  ( 0.000000000000000000, 0.000000000000000000, 65.00000000000000000 ) ) ;
#62497=FACE_OUTER_BOUND ( 'NONE', #80833, .T. ) ;
#62512=DIRECTION ( 'NONE',  ( -0.000000000000000000, -1.000000000000000000, -0.000000000000000000 ) ) ;
#62523=SURFACE_STYLE_FILL_AREA ( #63046 ) ;
#62552=EDGE_LOOP ( 'NONE', ( #22742, #37297 ) ) ;
#62761=DIRECTION ( 'NONE',  ( 0.000000000000000000, 0.000000000000000000, 1.000000000000000000 ) ) ;
#62859=DIRECTION ( 'NONE',  ( 0.000000000000000000, 0.000000000000000000, -1.000000000000000000 ) ) ;
#62964=EDGE_LOOP ( 'NONE', ( #77731, #90688, #95596, #42864 ) ) ;
#63046=FILL_AREA_STYLE ('',( #5853 ) ) ;
#63048=COLOUR_RGB ( '', 0.72549020, 0.75294118, 0.79215686) ;
#63118=SURFACE_STYLE_FILL_AREA ( #89515 ) ;
#63150=CIRCLE ( 'NONE', #42494, 61.50000000000000000 ) ;
#63177=FACE_OUTER_BOUND ( 'NONE', #60079, .T. ) ;
#63240=ORIENTED_EDGE ( 'NONE', *, *, #64281, .T. ) ;
#63278=SURFACE_STYLE_FILL_AREA ( #104244 ) ;
#63296=DIRECTION ( 'NONE',  ( 0.000000000000000000, 1.000000000000000000, 0.000000000000000000 ) ) ;
#63429=FACE_OUTER_BOUND ( 'NONE', #3836, .T. ) ;
#63508=CARTESIAN_POINT ( 'NONE',  ( 0.000000000000000000, 49.00000000000000000, 0.000000000000000000 ) ) ;
#63551=ADVANCED_FACE ( 'NONE', ( #76528 ), #85367, .F. ) ;
#63562=DIRECTION ( 'NONE',  ( 0.000000000000000000, 0.000000000000000000, 1.000000000000000000 ) ) ;
#63563=( LENGTH_UNIT ( ) NAMED_UNIT ( * ) SI_UNIT ( .MILLI., .METRE. ) );
#63567=EDGE_CURVE ( 'NONE', #92669, #75344, #46305, .T. ) ;
#63571=VERTEX_POINT ( 'NONE', #95384 ) ;
#63597=AXIS2_PLACEMENT_3D ( 'NONE', #76155, #98316, #26598 ) ;
#63645=EDGE_CURVE ( 'NONE', #89804, #41582, #4441, .T. ) ;
#63716=DIRECTION ( 'NONE',  ( 0.000000000000000000, 1.000000000000000000, 0.000000000000000000 ) ) ;
#63726=EDGE_CURVE ( 'NONE', #91723, #61967, #2665, .T. ) ;
#63811=SURFACE_SIDE_STYLE ('',( #63278 ) ) ;
#63931=SHAPE_REPRESENTATION ( '10. Furnel', ( #10728 ), #79579 ) ;
#63990=ADVANCED_FACE ( 'NONE', ( #71126 ), #57860, .T. ) ;
#64008=SURFACE_SIDE_STYLE ('',( #31121 ) ) ;
#64044=FACE_OUTER_BOUND ( 'NONE', #36700, .T. ) ;
#64149=EDGE_CURVE ( 'NONE', #1802, #14939, #78579, .T. ) ;
#64152=ORIENTED_EDGE ( 'NONE', *, *, #61853, .T. ) ;
#64185=ADVANCED_FACE ( 'NONE', ( #52158 ), #80341, .T. ) ;
#64186=EDGE_LOOP ( 'NONE', ( #77123, #16600, #31716, #10257 ) ) ;
#64238=EDGE_LOOP ( 'NONE', ( #24061, #29565 ) ) ;
#64273=SURFACE_STYLE_FILL_AREA ( #96631 ) ;
#64281=EDGE_CURVE ( 'NONE', #75344, #21876, #11432, .T. ) ;
#64353=DIRECTION ( 'NONE',  ( 1.000000000000000000, -0.000000000000000000, 1.224646799147353207E-16 ) ) ;
#64488=CARTESIAN_POINT ( 'NONE',  ( 0.000000000000000000, -0.5000000000000000000, 0.000000000000000000 ) ) ;
#64518=DIRECTION ( 'NONE',  ( 0.000000000000000000, 1.000000000000000000, 0.000000000000000000 ) ) ;
#64616=DIRECTION ( 'NONE',  ( -0.000000000000000000, -1.000000000000000000, -0.000000000000000000 ) ) ;
#64649=AXIS2_PLACEMENT_3D ( 'NONE', #70353, #62279, #95167 ) ;
#64688=LINE ( 'NONE', #13991, #54774 ) ;
#64775=DIRECTION ( 'NONE',  ( -0.000000000000000000, -1.000000000000000000, -0.000000000000000000 ) ) ;
#64782=CARTESIAN_POINT ( 'NONE',  ( 0.000000000000000000, -1.000000000000000000, 0.000000000000000000 ) ) ;
#64795=AXIS2_PLACEMENT_3D ( 'NONE', #13135, #54651, #14729 ) ;
#64836=EDGE_CURVE ( 'NONE', #63571, #87282, #66412, .T. ) ;
#64967=CARTESIAN_POINT ( 'NONE',  ( 0.000000000000000000, -15.00000000000000000, 0.000000000000000000 ) ) ;
#64998=DIRECTION ( 'NONE',  ( 0.000000000000000000, 1.000000000000000000, 0.000000000000000000 ) ) ;
#65236=EDGE_CURVE ( 'NONE', #77143, #106756, #7818, .T. ) ;
#65267=ORIENTED_EDGE ( 'NONE', *, *, #58110, .T. ) ;
#65430=ORIENTED_EDGE ( 'NONE', *, *, #66432, .T. ) ;
#65464=AXIS2_PLACEMENT_3D ( 'NONE', #45738, #53817, #12820 ) ;
#65649=ADVANCED_FACE ( 'NONE', ( #96392 ), #7887, .T. ) ;
#65670=DIRECTION ( 'NONE',  ( 1.000000000000000000, -0.000000000000000000, 1.224646799147353207E-16 ) ) ;
#65681=CARTESIAN_POINT ( 'NONE',  ( 1.836970198721029589E-15, 0.000000000000000000, -15.00000000000000000 ) ) ;
#65706=AXIS2_PLACEMENT_3D ( 'NONE', #102962, #62512, #61996 ) ;
#65756=ORIENTED_EDGE ( 'NONE', *, *, #63645, .T. ) ;
#65794=EDGE_CURVE ( 'NONE', #72311, #22326, #100899, .T. ) ;
#65838=ADVANCED_FACE ( 'NONE', ( #79479 ), #68274, .T. ) ;
#65844=STYLED_ITEM ( 'NONE', ( #50033 ), #74710 ) ;
#65864=FACE_BOUND ( 'NONE', #76768, .T. ) ;
#65867=AXIS2_PLACEMENT_3D ( 'NONE', #1691, #100396, #36774 ) ;
#65908=DIRECTION ( 'NONE',  ( 0.000000000000000000, 0.000000000000000000, 1.000000000000000000 ) ) ;
#65949=ORIENTED_EDGE ( 'NONE', *, *, #100237, .F. ) ;
#66070=VERTEX_POINT ( 'NONE', #98549 ) ;
#66163=ORIENTED_EDGE ( 'NONE', *, *, #57435, .F. ) ;
#66197=AXIS2_PLACEMENT_3D ( 'NONE', #64967, #31572, #13751 ) ;
#66371=DIRECTION ( 'NONE',  ( -0.000000000000000000, -1.000000000000000000, -0.000000000000000000 ) ) ;
#66412=CIRCLE ( 'NONE', #64649, 0.5000000000000004441 ) ;
#66432=EDGE_CURVE ( 'NONE', #14939, #1802, #20203, .T. ) ;
#66678=ORIENTED_EDGE ( 'NONE', *, *, #47857, .T. ) ;
#66681=DIRECTION ( 'NONE',  ( 0.000000000000000000, 0.000000000000000000, 1.000000000000000000 ) ) ;
#66741=( NAMED_UNIT ( * ) PLANE_ANGLE_UNIT ( ) SI_UNIT ( $, .RADIAN. ) );
#66827=DIRECTION ( 'NONE',  ( -0.000000000000000000, -1.000000000000000000, -0.000000000000000000 ) ) ;
#66916=CARTESIAN_POINT ( 'NONE',  ( 0.000000000000000000, 0.000000000000000000, 0.000000000000000000 ) ) ;
#66941=DIRECTION ( 'NONE',  ( 0.000000000000000000, -0.000000000000000000, 1.000000000000000000 ) ) ;
#66961=DIRECTION ( 'NONE',  ( 0.000000000000000000, 0.000000000000000000, -1.000000000000000000 ) ) ;
#67008=EDGE_CURVE ( 'NONE', #97780, #62139, #56377, .T. ) ;
#67011=FACE_OUTER_BOUND ( 'NONE', #74262, .T. ) ;
#67093=DIRECTION ( 'NONE',  ( 0.000000000000000000, 0.000000000000000000, 1.000000000000000000 ) ) ;
#67130=CIRCLE ( 'NONE', #103318, 0.5000000000000004441 ) ;
#67180=EDGE_CURVE ( 'NONE', #54015, #1507, #49487, .T. ) ;
#67251=AXIS2_PLACEMENT_3D ( 'NONE', #96569, #87947, #7523 ) ;
#67279=ADVANCED_FACE ( 'NONE', ( #10096, #19319 ), #43007, .F. ) ;
#67304=SURFACE_STYLE_FILL_AREA ( #68367 ) ;
#67413=AXIS2_PLACEMENT_3D ( 'NONE', #100633, #34877, #66681 ) ;
#67491=DIRECTION ( 'NONE',  ( -0.000000000000000000, -1.000000000000000000, -0.000000000000000000 ) ) ;
#67510=CARTESIAN_POINT ( 'NONE',  ( 0.000000000000000000, 45.00000000000000711, 59.50000000000000000 ) ) ;
#67706=AXIS2_PLACEMENT_3D ( 'NONE', #95381, #38749, #103469 ) ;
#67740=DIRECTION ( 'NONE',  ( 0.000000000000000000, 0.000000000000000000, 1.000000000000000000 ) ) ;
#67823=CARTESIAN_POINT ( 'NONE',  ( 0.000000000000000000, 0.000000000000000000, 0.000000000000000000 ) ) ;
#67875=DIRECTION ( 'NONE',  ( -1.000000000000000000, 0.000000000000000000, 0.000000000000000000 ) ) ;
#67947=MECHANICAL_DESIGN_GEOMETRIC_PRESENTATION_REPRESENTATION('',(#83417),#38700);
#67963=UNCERTAINTY_MEASURE_WITH_UNIT (LENGTH_MEASURE( 1.000000000000000082E-05 ), #23645, 'distance_accuracy_value', 'NONE');
#67990=CIRCLE ( 'NONE', #31821, 61.50000000000000000 ) ;
#68274=TOROIDAL_SURFACE ( 'NONE', #64795, 60.50000000000000000, 0.5000000000000000000 ) ;
#68367=FILL_AREA_STYLE ('',( #19332 ) ) ;
#68460=FILL_AREA_STYLE ('',( #35584 ) ) ;
#68538=AXIS2_PLACEMENT_3D ( 'NONE', #97994, #74244, #99037 ) ;
#68539=DIRECTION ( 'NONE',  ( -0.000000000000000000, -1.000000000000000000, -0.000000000000000000 ) ) ;
#68628=SURFACE_STYLE_FILL_AREA ( #21163 ) ;
#68741=PRESENTATION_STYLE_ASSIGNMENT (( #27243 ) ) ;
#68762=CARTESIAN_POINT ( 'NONE',  ( 0.000000000000000000, 79.50000000000000000, -65.50000000000000000 ) ) ;
#68942=( GEOMETRIC_REPRESENTATION_CONTEXT ( 3 ) GLOBAL_UNCERTAINTY_ASSIGNED_CONTEXT ( ( #2477 ) ) GLOBAL_UNIT_ASSIGNED_CONTEXT ( ( #87426, #7004, #22704 ) ) REPRESENTATION_CONTEXT ( 'NONE', 'WORKASPACE' ) );
#69109=CARTESIAN_POINT ( 'NONE',  ( 0.000000000000000000, -1.023477375540016387, 16.09658290236430389 ) ) ;
#69114=CIRCLE ( 'NONE', #65706, 9.000000000000000000 ) ;
#69131=MECHANICAL_DESIGN_GEOMETRIC_PRESENTATION_REPRESENTATION('',(#7120),#84595);
#69146=DIRECTION ( 'NONE',  ( 0.000000000000000000, -0.000000000000000000, 1.000000000000000000 ) ) ;
#69188=SURFACE_STYLE_FILL_AREA ( #20134 ) ;
#69195=SURFACE_SIDE_STYLE ('',( #51383 ) ) ;
#69367=ORIENTED_EDGE ( 'NONE', *, *, #44560, .F. ) ;
#69386=PLANE ( 'NONE',  #28512 ) ;
#69432=ADVANCED_FACE ( 'NONE', ( #30676 ), #82571, .F. ) ;
#69464=CIRCLE ( 'NONE', #91856, 10.00000000000000000 ) ;
#69566=AXIS2_PLACEMENT_3D ( 'NONE', #5464, #22738, #55577 ) ;
#69580=ORIENTED_EDGE ( 'NONE', *, *, #31899, .T. ) ;
#69724=CARTESIAN_POINT ( 'NONE',  ( 1.224646799147353256E-15, -1.500000000000000000, -10.00000000000000000 ) ) ;
#69887=ORIENTED_EDGE ( 'NONE', *, *, #93246, .T. ) ;
#69909=FACE_BOUND ( 'NONE', #59276, .T. ) ;
#70038=PLANE ( 'NONE',  #46443 ) ;
#70060=CARTESIAN_POINT ( 'NONE',  ( 0.000000000000000000, 49.50000000000000000, 0.000000000000000000 ) ) ;
#70235=( NAMED_UNIT ( * ) SI_UNIT ( $, .STERADIAN. ) SOLID_ANGLE_UNIT ( ) );
#70254=AXIS2_PLACEMENT_3D ( 'NONE', #57124, #14534, #38847 ) ;
#70281=DIRECTION ( 'NONE',  ( 0.000000000000000000, 0.000000000000000000, 1.000000000000000000 ) ) ;
#70322=SURFACE_STYLE_FILL_AREA ( #78399 ) ;
#70353=CARTESIAN_POINT ( 'NONE',  ( 0.000000000000000000, 48.00000000000000000, 62.00000000000000000 ) ) ;
#70417=DIRECTION ( 'NONE',  ( 0.000000000000000000, 0.000000000000000000, -1.000000000000000000 ) ) ;
#70428=CARTESIAN_POINT ( 'NONE',  ( 0.000000000000000000, 79.50000000000000000, 0.000000000000000000 ) ) ;
#70449=( GEOMETRIC_REPRESENTATION_CONTEXT ( 3 ) GLOBAL_UNCERTAINTY_ASSIGNED_CONTEXT ( ( #87406 ) ) GLOBAL_UNIT_ASSIGNED_CONTEXT ( ( #16586, #96978, #24705 ) ) REPRESENTATION_CONTEXT ( 'NONE', 'WORKASPACE' ) );
#70467=EDGE_CURVE ( 'NONE', #21786, #66070, #72332, .T. ) ;
#70519=TOROIDAL_SURFACE ( 'NONE', #32671, 15.43455230191221261, 0.5000000000000000000 ) ;
#70526=CARTESIAN_POINT ( 'NONE',  ( 0.000000000000000000, 80.00000000000000000, 0.000000000000000000 ) ) ;
#70567=EDGE_LOOP ( 'NONE', ( #65430, #58376 ) ) ;
#70652=ORIENTED_EDGE ( 'NONE', *, *, #51710, .T. ) ;
#70730=EDGE_CURVE ( 'NONE', #72311, #41058, #39705, .T. ) ;
#70778=CARTESIAN_POINT ( 'NONE',  ( 0.000000000000000000, -15.00000000000000000, 0.000000000000000000 ) ) ;
#70810=DIRECTION ( 'NONE',  ( 0.000000000000000000, 1.000000000000000000, 0.000000000000000000 ) ) ;
#70848=CARTESIAN_POINT ( 'NONE',  ( 1.163414459189985485E-15, -14.49999999999999822, -9.500000000000000000 ) ) ;
#70922=CARTESIAN_POINT ( 'NONE',  ( 0.000000000000000000, -15.00000000000000000, 0.000000000000000000 ) ) ;
#70924=AXIS2_PLACEMENT_3D ( 'NONE', #103005, #13965, #46873 ) ;
#71004=CIRCLE ( 'NONE', #83015, 61.00000000000000000 ) ;
#71018=LINE ( 'NONE', #5233, #51055 ) ;
#71126=FACE_OUTER_BOUND ( 'NONE', #74676, .T. ) ;
#71228=CARTESIAN_POINT ( 'NONE',  ( 0.000000000000000000, 44.84115912518001323, 0.000000000000000000 ) ) ;
#71321=DIRECTION ( 'NONE',  ( 0.000000000000000000, 1.000000000000000000, 0.000000000000000000 ) ) ;
#71345=FILL_AREA_STYLE_COLOUR ( '', #81379 ) ;
#71354=DIRECTION ( 'NONE',  ( 0.000000000000000000, 0.000000000000000000, 1.000000000000000000 ) ) ;
#71402=ORIENTED_EDGE ( 'NONE', *, *, #63567, .F. ) ;
#71536=DIRECTION ( 'NONE',  ( 0.000000000000000000, 0.000000000000000000, -1.000000000000000000 ) ) ;
#71578=FILL_AREA_STYLE_COLOUR ( '', #24134 ) ;
#71646=CIRCLE ( 'NONE', #25193, 64.50000000000000000 ) ;
#71700=ORIENTED_EDGE ( 'NONE', *, *, #103543, .F. ) ;
#71766=DIRECTION ( 'NONE',  ( 1.224646799147349509E-16, 0.000000000000000000, -1.000000000000000000 ) ) ;
#71894=DIRECTION ( 'NONE',  ( 0.000000000000000000, 1.000000000000000000, 0.000000000000000000 ) ) ;
#71897=CYLINDRICAL_SURFACE ( 'NONE', #38165, 8.000000000000000000 ) ;
#71948=TOROIDAL_SURFACE ( 'NONE', #70254, 8.500000000000000000, 0.5000000000000000000 ) ;
#71983=ORIENTED_EDGE ( 'NONE', *, *, #1490, .F. ) ;
#71990=CARTESIAN_POINT ( 'NONE',  ( 0.000000000000000000, 0.000000000000000000, 9.500000000000000000 ) ) ;
#72012=AXIS2_PLACEMENT_3D ( 'NONE', #59829, #52241, #84624 ) ;
#72104=EDGE_CURVE ( 'NONE', #21876, #75344, #53393, .T. ) ;
#72125=ORIENTED_EDGE ( 'NONE', *, *, #28770, .T. ) ;
#72172=ORIENTED_EDGE ( 'NONE', *, *, #31899, .F. ) ;
#72181=CLOSED_SHELL ( 'NONE', ( #15930, #80288, #86480, #25413, #59080, #74710, #63990, #52429, #84035, #82163, #33406, #19825, #19983, #38645, #64185, #32877, #99983, #28445, #65649, #40506, #28689, #98436, #78853, #50726, #67279, #59846, #637, #72819, #29848, #48707, #59269, #10012, #89573, #42205, #33736, #12436, #100563, #30650, #102283, #51795, #30111, #55430, #74929, #65838, #69432, #19602, #105482, #34362, #53583, #1907, #40448, #63551, #20943, #46250, #98311, #21784 ) ) ;
#72231=EDGE_LOOP ( 'NONE', ( #106716, #53582, #106441, #53257 ) ) ;
#72311=VERTEX_POINT ( 'NONE', #102119 ) ;
#72316=DIRECTION ( 'NONE',  ( 0.000000000000000000, 0.000000000000000000, 1.000000000000000000 ) ) ;
#72332=CIRCLE ( 'NONE', #29347, 9.500000000000000000 ) ;
#72348=FILL_AREA_STYLE_COLOUR ( '', #85544 ) ;
#72430=( NAMED_UNIT ( * ) SI_UNIT ( $, .STERADIAN. ) SOLID_ANGLE_UNIT ( ) );
#72568=DIRECTION ( 'NONE',  ( 0.000000000000000000, 1.000000000000000000, 0.000000000000000000 ) ) ;
#72593=DIRECTION ( 'NONE',  ( -0.000000000000000000, -1.000000000000000000, -0.000000000000000000 ) ) ;
#72644=CARTESIAN_POINT ( 'NONE',  ( 0.000000000000000000, -2.000000000000000000, 9.500000000000000000 ) ) ;
#72692=DIRECTION ( 'NONE',  ( 1.224646799147349509E-16, 0.000000000000000000, -1.000000000000000000 ) ) ;
#72712=CIRCLE ( 'NONE', #81326, 0.5000000000000004441 ) ;
#72732=ORIENTED_EDGE ( 'NONE', *, *, #25340, .T. ) ;
#72746=AXIS2_PLACEMENT_3D ( 'NONE', #21563, #29668, #88931 ) ;
#72819=ADVANCED_FACE ( 'NONE', ( #67011, #2786 ), #19562, .T. ) ;
#72821=VERTEX_POINT ( 'NONE', #83699 ) ;
#72851=( NAMED_UNIT ( * ) PLANE_ANGLE_UNIT ( ) SI_UNIT ( $, .RADIAN. ) );
#72995=CIRCLE ( 'NONE', #69566, 65.00000000000000000 ) ;
#73056=ORIENTED_EDGE ( 'NONE', *, *, #13948, .T. ) ;
#73149=ORIENTED_EDGE ( 'NONE', *, *, #14992, .T. ) ;
#73186=AXIS2_PLACEMENT_3D ( 'NONE', #41374, #82898, #57012 ) ;
#73291=PRODUCT_DEFINITION ( 'UNKNOWN', '', #100734, #52092 ) ;
#73436=DIRECTION ( 'NONE',  ( -0.000000000000000000, -1.000000000000000000, -0.000000000000000000 ) ) ;
#73455=CARTESIAN_POINT ( 'NONE',  ( 0.000000000000000000, -15.00000000000000000, -9.000000000000000000 ) ) ;
#73526=AXIS2_PLACEMENT_3D ( 'NONE', #5133, #23462, #21875 ) ;
#73531=ORIENTED_EDGE ( 'NONE', *, *, #56973, .F. ) ;
#73621=VERTEX_POINT ( 'NONE', #22061 ) ;
#73673=EDGE_CURVE ( 'NONE', #38219, #59944, #8795, .T. ) ;
#73686=CYLINDRICAL_SURFACE ( 'NONE', #25239, 61.50000000000000000 ) ;
#73687=VERTEX_POINT ( 'NONE', #95938 ) ;
#73725=EDGE_CURVE ( 'NONE', #72821, #12582, #69114, .T. ) ;
#73989=DIRECTION ( 'NONE',  ( -1.000000000000000000, 0.000000000000000000, 0.000000000000000000 ) ) ;
#74053=MECHANICAL_DESIGN_GEOMETRIC_PRESENTATION_REPRESENTATION('',(#25849),#25933);
#74088=VERTEX_POINT ( 'NONE', #38140 ) ;
#74143=DIRECTION ( 'NONE',  ( 0.000000000000000000, 1.000000000000000000, 0.000000000000000000 ) ) ;
#74162=CARTESIAN_POINT ( 'NONE',  ( 7.042157147547021781E-15, 43.34115912517999902, -57.50357696970298349 ) ) ;
#74244=DIRECTION ( 'NONE',  ( -0.000000000000000000, -1.000000000000000000, -0.000000000000000000 ) ) ;
#74262=EDGE_LOOP ( 'NONE', ( #100085, #1920 ) ) ;
#74287=( NAMED_UNIT ( * ) SI_UNIT ( $, .STERADIAN. ) SOLID_ANGLE_UNIT ( ) );
#74303=CARTESIAN_POINT ( 'NONE',  ( 0.000000000000000000, 79.50000000000000000, 0.000000000000000000 ) ) ;
#74310=CARTESIAN_POINT ( 'NONE',  ( 0.000000000000000000, 0.000000000000000000, 60.00000000000000000 ) ) ;
#74360=CARTESIAN_POINT ( 'NONE',  ( 0.000000000000000000, 0.5000000000000000000, 0.000000000000000000 ) ) ;
#74595=STYLED_ITEM ( 'NONE', ( #55861 ), #84035 ) ;
#74676=EDGE_LOOP ( 'NONE', ( #37576, #57662, #53694, #91875 ) ) ;
#74710=ADVANCED_FACE ( 'NONE', ( #34434 ), #22765, .T. ) ;
#74782=FACE_OUTER_BOUND ( 'NONE', #28307, .T. ) ;
#74827=DIRECTION ( 'NONE',  ( 0.000000000000000000, 0.000000000000000000, -1.000000000000000000 ) ) ;
#74864=ORIENTED_EDGE ( 'NONE', *, *, #35218, .T. ) ;
#74889=CARTESIAN_POINT ( 'NONE',  ( 0.000000000000000000, 43.50000000000000711, 0.000000000000000000 ) ) ;
#74924=CIRCLE ( 'NONE', #21548, 0.5000000000000004441 ) ;
#74929=ADVANCED_FACE ( 'NONE', ( #53761 ), #31394, .T. ) ;
#74968=EDGE_LOOP ( 'NONE', ( #102002, #53589, #89991, #51585 ) ) ;
#74977=CYLINDRICAL_SURFACE ( 'NONE', #61917, 9.500000000000000000 ) ;
#74984=CARTESIAN_POINT ( 'NONE',  ( 0.000000000000000000, -0.5000000000000000000, 8.000000000000000000 ) ) ;
#74985=CARTESIAN_POINT ( 'NONE',  ( 0.000000000000000000, -0.5000000000000000000, 0.000000000000000000 ) ) ;
#75192=MECHANICAL_DESIGN_GEOMETRIC_PRESENTATION_REPRESENTATION('',(#44195),#76971);
#75201=ORIENTED_EDGE ( 'NONE', *, *, #46332, .F. ) ;
#75223=DIRECTION ( 'NONE',  ( -1.000000000000000000, 0.000000000000000000, 0.000000000000000000 ) ) ;
#75344=VERTEX_POINT ( 'NONE', #4030 ) ;
#75460=VERTEX_POINT ( 'NONE', #87613 ) ;
#75510=CIRCLE ( 'NONE', #4928, 0.5000000000000004441 ) ;
#75550=AXIS2_PLACEMENT_3D ( 'NONE', #58277, #51230, #49107 ) ;
#75569=CARTESIAN_POINT ( 'NONE',  ( 0.000000000000000000, 50.50000000000000000, 0.000000000000000000 ) ) ;
#75750=EDGE_LOOP ( 'NONE', ( #11768, #57401 ) ) ;
#75867=ORIENTED_EDGE ( 'NONE', *, *, #67008, .T. ) ;
#75896=DIRECTION ( 'NONE',  ( 0.000000000000000000, 0.000000000000000000, -1.000000000000000000 ) ) ;
#76018=CARTESIAN_POINT ( 'NONE',  ( 1.163414459189985485E-15, -2.000000000000000000, -9.500000000000000000 ) ) ;
#76072=ORIENTED_EDGE ( 'NONE', *, *, #64281, .F. ) ;
#76103=EDGE_CURVE ( 'NONE', #75460, #99989, #13489, .T. ) ;
#76142=CARTESIAN_POINT ( 'NONE',  ( 0.000000000000000000, 0.000000000000000000, -8.000000000000000000 ) ) ;
#76155=CARTESIAN_POINT ( 'NONE',  ( 0.000000000000000000, -14.49999999999999822, 0.000000000000000000 ) ) ;
#76243=ORIENTED_EDGE ( 'NONE', *, *, #32591, .T. ) ;
#76361=CARTESIAN_POINT ( 'NONE',  ( 0.000000000000000000, 49.00000000000000000, 0.000000000000000000 ) ) ;
#76407=CARTESIAN_POINT ( 'NONE',  ( 0.000000000000000000, 45.00000000000000711, 0.000000000000000000 ) ) ;
#76528=FACE_OUTER_BOUND ( 'NONE', #77617, .T. ) ;
#76745=AXIS2_PLACEMENT_3D ( 'NONE', #63508, #14385, #105017 ) ;
#76768=EDGE_LOOP ( 'NONE', ( #95375, #106494 ) ) ;
#76905=UNCERTAINTY_MEASURE_WITH_UNIT (LENGTH_MEASURE( 1.000000000000000082E-05 ), #98561, 'distance_accuracy_value', 'NONE');
#76945=ORIENTED_EDGE ( 'NONE', *, *, #93514, .F. ) ;
#76971=( GEOMETRIC_REPRESENTATION_CONTEXT ( 3 ) GLOBAL_UNCERTAINTY_ASSIGNED_CONTEXT ( ( #86095 ) ) GLOBAL_UNIT_ASSIGNED_CONTEXT ( ( #79374, #104176, #103655 ) ) REPRESENTATION_CONTEXT ( 'NONE', 'WORKASPACE' ) );
#76982=DIRECTION ( 'NONE',  ( 0.000000000000000000, 0.000000000000000000, 1.000000000000000000 ) ) ;
#77093=DIRECTION ( 'NONE',  ( 1.224646799147349509E-16, 0.000000000000000000, -1.000000000000000000 ) ) ;
#77123=ORIENTED_EDGE ( 'NONE', *, *, #39352, .F. ) ;
#77132=MECHANICAL_DESIGN_GEOMETRIC_PRESENTATION_REPRESENTATION('',(#18655),#94394);
#77143=VERTEX_POINT ( 'NONE', #76018 ) ;
#77189=MECHANICAL_DESIGN_GEOMETRIC_PRESENTATION_REPRESENTATION('',(#4815),#94366);
#77284=CIRCLE ( 'NONE', #42867, 57.21727615095610275 ) ;
#77482=VERTEX_POINT ( 'NONE', #74162 ) ;
#77507=DIRECTION ( 'NONE',  ( 0.000000000000000000, 0.000000000000000000, 1.000000000000000000 ) ) ;
#77595=CIRCLE ( 'NONE', #48306, 0.5000000000000004441 ) ;
#77617=EDGE_LOOP ( 'NONE', ( #15947, #33189, #45865, #23695 ) ) ;
#77631=CARTESIAN_POINT ( 'NONE',  ( 7.470345474798855081E-15, 44.00000000000000711, -61.00000000000000000 ) ) ;
#77677=DIRECTION ( 'NONE',  ( 0.000000000000000000, 0.000000000000000000, 1.000000000000000000 ) ) ;
#77701=( NAMED_UNIT ( * ) SI_UNIT ( $, .STERADIAN. ) SOLID_ANGLE_UNIT ( ) );
#77723=LINE ( 'NONE', #69109, #105859 ) ;
#77731=ORIENTED_EDGE ( 'NONE', *, *, #20001, .F. ) ;
#77831=ORIENTED_EDGE ( 'NONE', *, *, #70730, .F. ) ;
#77879=CIRCLE ( 'NONE', #31391, 0.5000000000000004441 ) ;
#78068=CARTESIAN_POINT ( 'NONE',  ( 0.000000000000000000, -14.49999999999999822, 8.000000000000000000 ) ) ;
#78100=ORIENTED_EDGE ( 'NONE', *, *, #57577, .T. ) ;
#78194=FILL_AREA_STYLE_COLOUR ( '', #105299 ) ;
#78282=FACE_OUTER_BOUND ( 'NONE', #96163, .T. ) ;
#78296=DIRECTION ( 'NONE',  ( 0.000000000000000000, 0.000000000000000000, 1.000000000000000000 ) ) ;
#78399=FILL_AREA_STYLE ('',( #45526 ) ) ;
#78461=LINE ( 'NONE', #27306, #33665 ) ;
#78537=DIRECTION ( 'NONE',  ( 0.000000000000000000, 1.000000000000000000, 0.000000000000000000 ) ) ;
#78560=CARTESIAN_POINT ( 'NONE',  ( 0.000000000000000000, 44.50000000000000711, 0.000000000000000000 ) ) ;
#78570=SURFACE_SIDE_STYLE ('',( #14353 ) ) ;
#78579=CIRCLE ( 'NONE', #1015, 8.500000000000000000 ) ;
#78615=CARTESIAN_POINT ( 'NONE',  ( 0.000000000000000000, 0.000000000000000000, 0.000000000000000000 ) ) ;
#78676=SURFACE_SIDE_STYLE ('',( #62523 ) ) ;
#78732=EDGE_CURVE ( 'NONE', #15446, #38219, #41417, .T. ) ;
#78735=SURFACE_STYLE_FILL_AREA ( #37270 ) ;
#78826=CARTESIAN_POINT ( 'NONE',  ( 0.000000000000000000, -2.000000000000000000, 0.000000000000000000 ) ) ;
#78847=AXIS2_PLACEMENT_3D ( 'NONE', #3431, #43878, #60627 ) ;
#78853=ADVANCED_FACE ( 'NONE', ( #43024 ), #87965, .F. ) ;
#78856=FACE_BOUND ( 'NONE', #44456, .T. ) ;
#78986=DIRECTION ( 'NONE',  ( 0.000000000000000000, 1.000000000000000000, 0.000000000000000000 ) ) ;
#79098=CARTESIAN_POINT ( 'NONE',  ( 0.000000000000000000, -1.000000000000000000, 0.000000000000000000 ) ) ;
#79126=( GEOMETRIC_REPRESENTATION_CONTEXT ( 3 ) GLOBAL_UNCERTAINTY_ASSIGNED_CONTEXT ( ( #31224 ) ) GLOBAL_UNIT_ASSIGNED_CONTEXT ( ( #21703, #72851, #103648 ) ) REPRESENTATION_CONTEXT ( 'NONE', 'WORKASPACE' ) );
#79180=DIRECTION ( 'NONE',  ( 0.000000000000000000, 0.000000000000000000, 1.000000000000000000 ) ) ;
#79230=ORIENTED_EDGE ( 'NONE', *, *, #63726, .T. ) ;
#79236=LINE ( 'NONE', #30175, #90008 ) ;
#79325=AXIS2_PLACEMENT_3D ( 'NONE', #60296, #44632, #91582 ) ;
#79343=FILL_AREA_STYLE_COLOUR ( '', #24926 ) ;
#79374=( LENGTH_UNIT ( ) NAMED_UNIT ( * ) SI_UNIT ( .MILLI., .METRE. ) );
#79479=FACE_OUTER_BOUND ( 'NONE', #103047, .T. ) ;
#79579=( GEOMETRIC_REPRESENTATION_CONTEXT ( 3 ) GLOBAL_UNCERTAINTY_ASSIGNED_CONTEXT ( ( #67963 ) ) GLOBAL_UNIT_ASSIGNED_CONTEXT ( ( #23645, #19314, #60276 ) ) REPRESENTATION_CONTEXT ( 'NONE', 'WORKASPACE' ) );
#79588=CARTESIAN_POINT ( 'NONE',  ( 0.000000000000000000, 43.50000000000000711, 0.000000000000000000 ) ) ;
#79706=AXIS2_PLACEMENT_3D ( 'NONE', #8205, #98282, #50770 ) ;
#79763=DIRECTION ( 'NONE',  ( 0.000000000000000000, 1.000000000000000000, 0.000000000000000000 ) ) ;
#79764=MECHANICAL_DESIGN_GEOMETRIC_PRESENTATION_REPRESENTATION('',(#5713),#88407);
#79891=SURFACE_STYLE_USAGE ( .BOTH. , #6529 ) ;
#79907=AXIS2_PLACEMENT_3D ( 'NONE', #39651, #104355, #56857 ) ;
#80087=DIRECTION ( 'NONE',  ( 0.000000000000000000, 1.000000000000000000, 0.000000000000000000 ) ) ;
#80217=SURFACE_SIDE_STYLE ('',( #29596 ) ) ;
#80282=VERTEX_POINT ( 'NONE', #56064 ) ;
#80288=ADVANCED_FACE ( 'NONE', ( #14029 ), #46522, .F. ) ;
#80341=TOROIDAL_SURFACE ( 'NONE', #94149, 65.50000000000000000, 0.5000000000000000000 ) ;
#80429=CIRCLE ( 'NONE', #106220, 0.5000000000000004441 ) ;
#80730=EDGE_CURVE ( 'NONE', #2579, #87282, #87694, .T. ) ;
#80755=ORIENTED_EDGE ( 'NONE', *, *, #37106, .F. ) ;
#80833=EDGE_LOOP ( 'NONE', ( #62474, #78100, #81319, #63240 ) ) ;
#80892=DIRECTION ( 'NONE',  ( 1.000000000000000000, -0.000000000000000000, 1.224646799147353207E-16 ) ) ;
#80956=PRESENTATION_STYLE_ASSIGNMENT (( #88013 ) ) ;
#80984=ORIENTED_EDGE ( 'NONE', *, *, #10539, .F. ) ;
#81011=AXIS2_PLACEMENT_3D ( 'NONE', #76142, #1162, #69146 ) ;
#81126=CYLINDRICAL_SURFACE ( 'NONE', #54355, 66.50000000000000000 ) ;
#81300=SURFACE_SIDE_STYLE ('',( #6894 ) ) ;
#81319=ORIENTED_EDGE ( 'NONE', *, *, #63567, .T. ) ;
#81326=AXIS2_PLACEMENT_3D ( 'NONE', #50253, #73989, #65908 ) ;
#81379=COLOUR_RGB ( '', 0.66274510, 0.83137255, 0.94901961) ;
#81469=EDGE_LOOP ( 'NONE', ( #4802, #31987, #103705, #72172 ) ) ;
#81505=DIRECTION ( 'NONE',  ( 0.000000000000000000, 1.000000000000000000, 0.000000000000000000 ) ) ;
#81842=ORIENTED_EDGE ( 'NONE', *, *, #91719, .F. ) ;
#82134=SHAPE_DEFINITION_REPRESENTATION ( #51766, #63931 ) ;
#82163=ADVANCED_FACE ( 'NONE', ( #26333 ), #15708, .T. ) ;
#82220=MECHANICAL_DESIGN_GEOMETRIC_PRESENTATION_REPRESENTATION('',(#13301),#96018);
#82284=VECTOR ( 'NONE', #78537, 1000.000000000000000 ) ;
#82445=EDGE_LOOP ( 'NONE', ( #2629, #24220 ) ) ;
#82450=CARTESIAN_POINT ( 'NONE',  ( 8.143901214329899974E-15, 79.50000000000000000, -66.50000000000000000 ) ) ;
#82522=COLOUR_RGB ( '', 0.40784314, 0.44705882, 0.49803922) ;
#82571=TOROIDAL_SURFACE ( 'NONE', #103300, 59.50000000000000000, 0.5000000000000000000 ) ;
#82623=COLOUR_RGB ( '', 0.72549020, 0.75294118, 0.79215686) ;
#82684=TOROIDAL_SURFACE ( 'NONE', #60312, 61.00000000000000000, 0.5000000000000000000 ) ;
#82699=EDGE_LOOP ( 'NONE', ( #31610, #105236, #41151, #19507 ) ) ;
#82789=CIRCLE ( 'NONE', #91430, 65.50000000000000000 ) ;
#82898=DIRECTION ( 'NONE',  ( 0.000000000000000000, 1.000000000000000000, 0.000000000000000000 ) ) ;
#82969=CIRCLE ( 'NONE', #36524, 0.5000000000000004441 ) ;
#83015=AXIS2_PLACEMENT_3D ( 'NONE', #74889, #66827, #25887 ) ;
#83020=VERTEX_POINT ( 'NONE', #49625 ) ;
#83175=MECHANICAL_DESIGN_GEOMETRIC_PRESENTATION_REPRESENTATION('',(#102109),#17742);
#83237=CIRCLE ( 'NONE', #50513, 0.5000000000000004441 ) ;
#83250=ORIENTED_EDGE ( 'NONE', *, *, #11628, .F. ) ;
#83271=AXIS2_PLACEMENT_3D ( 'NONE', #106234, #57159, #90071 ) ;
#83380=CARTESIAN_POINT ( 'NONE',  ( 0.000000000000000000, 0.000000000000000000, 0.000000000000000000 ) ) ;
#83390=DIRECTION ( 'NONE',  ( 0.000000000000000000, 0.000000000000000000, 1.000000000000000000 ) ) ;
#83417=STYLED_ITEM ( 'NONE', ( #52949 ), #98311 ) ;
#83441=DIRECTION ( 'NONE',  ( -0.000000000000000000, -1.000000000000000000, -0.000000000000000000 ) ) ;
#83444=FILL_AREA_STYLE_COLOUR ( '', #33103 ) ;
#83699=CARTESIAN_POINT ( 'NONE',  ( 1.132798289211301501E-15, -15.00000000000000000, 9.000000000000000000 ) ) ;
#83804=DIRECTION ( 'NONE',  ( 0.000000000000000000, 1.000000000000000000, 0.000000000000000000 ) ) ;
#83847=CARTESIAN_POINT ( 'NONE',  ( 0.000000000000000000, 50.00000000000000000, 0.000000000000000000 ) ) ;
#83913=FACE_OUTER_BOUND ( 'NONE', #100557, .T. ) ;
#83980=SURFACE_SIDE_STYLE ('',( #93144 ) ) ;
#84035=ADVANCED_FACE ( 'NONE', ( #87218 ), #52195, .T. ) ;
#84130=EDGE_CURVE ( 'NONE', #60249, #160, #69464, .T. ) ;
#84139=AXIS2_PLACEMENT_3D ( 'NONE', #71228, #4916, #21138 ) ;
#84162=CIRCLE ( 'NONE', #15257, 0.5000000000000004441 ) ;
#84298=PRESENTATION_STYLE_ASSIGNMENT (( #2293 ) ) ;
#84354=CARTESIAN_POINT ( 'NONE',  ( 0.000000000000000000, 80.00000000000000000, 0.000000000000000000 ) ) ;
#84383=VERTEX_POINT ( 'NONE', #74984 ) ;
#84392=DIRECTION ( 'NONE',  ( 0.000000000000000000, 0.000000000000000000, 1.000000000000000000 ) ) ;
#84513=ORIENTED_EDGE ( 'NONE', *, *, #76103, .F. ) ;
#84544=DIRECTION ( 'NONE',  ( -0.000000000000000000, -1.000000000000000000, -0.000000000000000000 ) ) ;
#84595=( GEOMETRIC_REPRESENTATION_CONTEXT ( 3 ) GLOBAL_UNCERTAINTY_ASSIGNED_CONTEXT ( ( #40760 ) ) GLOBAL_UNIT_ASSIGNED_CONTEXT ( ( #47275, #28094, #60450 ) ) REPRESENTATION_CONTEXT ( 'NONE', 'WORKASPACE' ) );
#84605=DIRECTION ( 'NONE',  ( 0.000000000000000000, 0.000000000000000000, 1.000000000000000000 ) ) ;
#84624=DIRECTION ( 'NONE',  ( 0.000000000000000000, 0.000000000000000000, 1.000000000000000000 ) ) ;
#84823=DIRECTION ( 'NONE',  ( 0.000000000000000000, 0.000000000000000000, 1.000000000000000000 ) ) ;
#84895=ORIENTED_EDGE ( 'NONE', *, *, #89055, .F. ) ;
#84910=VERTEX_POINT ( 'NONE', #78068 ) ;
#84916=DIRECTION ( 'NONE',  ( 0.000000000000000000, 0.000000000000000000, 1.000000000000000000 ) ) ;
#85043=CARTESIAN_POINT ( 'NONE',  ( 7.086921372259695358E-15, 43.00000000000000000, -57.86910460382442523 ) ) ;
#85057=FILL_AREA_STYLE ('',( #83444 ) ) ;
#85063=DIRECTION ( 'NONE',  ( 0.000000000000000000, -1.000000000000000000, -0.000000000000000000 ) ) ;
#85173=EDGE_LOOP ( 'NONE', ( #65756, #66678 ) ) ;
#85238=DIRECTION ( 'NONE',  ( 0.000000000000000000, 0.000000000000000000, 1.000000000000000000 ) ) ;
#85288=DIRECTION ( 'NONE',  ( 0.000000000000000000, 1.000000000000000000, 0.000000000000000000 ) ) ;
#85294=EDGE_CURVE ( 'NONE', #19286, #22326, #43810, .T. ) ;
#85354=( NAMED_UNIT ( * ) PLANE_ANGLE_UNIT ( ) SI_UNIT ( $, .RADIAN. ) );
#85367=TOROIDAL_SURFACE ( 'NONE', #33729, 10.00000000000000000, 0.5000000000000000000 ) ;
#85544=COLOUR_RGB ( '', 0.08235294, 0.09019608, 0.10196078) ;
#85601=( LENGTH_UNIT ( ) NAMED_UNIT ( * ) SI_UNIT ( .MILLI., .METRE. ) );
#85654=ORIENTED_EDGE ( 'NONE', *, *, #105400, .T. ) ;
#85692=EDGE_CURVE ( 'NONE', #99989, #50441, #77723, .T. ) ;
#85712=DIRECTION ( 'NONE',  ( 0.000000000000000000, -0.000000000000000000, 1.000000000000000000 ) ) ;
#85735=ORIENTED_EDGE ( 'NONE', *, *, #51829, .T. ) ;
#85964=ORIENTED_EDGE ( 'NONE', *, *, #78732, .T. ) ;
#85966=TOROIDAL_SURFACE ( 'NONE', #42894, 64.50000000000000000, 0.5000000000000000000 ) ;
#86095=UNCERTAINTY_MEASURE_WITH_UNIT (LENGTH_MEASURE( 1.000000000000000082E-05 ), #79374, 'distance_accuracy_value', 'NONE');
#86257=CIRCLE ( 'NONE', #103400, 66.50000000000000000 ) ;
#86269=ORIENTED_EDGE ( 'NONE', *, *, #34890, .F. ) ;
#86345=( LENGTH_UNIT ( ) NAMED_UNIT ( * ) SI_UNIT ( .MILLI., .METRE. ) );
#86411=DIRECTION ( 'NONE',  ( 0.000000000000000000, 0.000000000000000000, 1.000000000000000000 ) ) ;
#86429=( GEOMETRIC_REPRESENTATION_CONTEXT ( 3 ) GLOBAL_UNCERTAINTY_ASSIGNED_CONTEXT ( ( #76905 ) ) GLOBAL_UNIT_ASSIGNED_CONTEXT ( ( #98561, #66741, #74287 ) ) REPRESENTATION_CONTEXT ( 'NONE', 'WORKASPACE' ) );
#86480=ADVANCED_FACE ( 'NONE', ( #23080 ), #87096, .T. ) ;
#86531=DIRECTION ( 'NONE',  ( 0.000000000000000000, 0.000000000000000000, 1.000000000000000000 ) ) ;
#86576=DIRECTION ( 'NONE',  ( 0.000000000000000000, 0.000000000000000000, 1.000000000000000000 ) ) ;
#86661=TOROIDAL_SURFACE ( 'NONE', #46959, 14.78272384904389192, 0.5000000000000000000 ) ;
#86680=DIRECTION ( 'NONE',  ( -1.000000000000000000, 0.000000000000000000, 0.000000000000000000 ) ) ;
#86724=ORIENTED_EDGE ( 'NONE', *, *, #53947, .T. ) ;
#86748=FACE_OUTER_BOUND ( 'NONE', #49169, .T. ) ;
#86903=TOROIDAL_SURFACE ( 'NONE', #52446, 62.00000000000000000, 0.5000000000000000000 ) ;
#86906=EDGE_CURVE ( 'NONE', #74088, #77482, #47412, .T. ) ;
#86959=FACE_OUTER_BOUND ( 'NONE', #27575, .T. ) ;
#86965=DIRECTION ( 'NONE',  ( 0.000000000000000000, 1.000000000000000000, 0.000000000000000000 ) ) ;
#86968=CARTESIAN_POINT ( 'NONE',  ( 0.000000000000000000, 45.00000000000000711, 0.000000000000000000 ) ) ;
#87030=FACE_OUTER_BOUND ( 'NONE', #61688, .T. ) ;
#87096=TOROIDAL_SURFACE ( 'NONE', #54328, 61.00000000000000000, 0.5000000000000000000 ) ;
#87123=CYLINDRICAL_SURFACE ( 'NONE', #73526, 65.00000000000000000 ) ;
#87137=CARTESIAN_POINT ( 'NONE',  ( 6.962331184707186918E-15, 44.84115912518001323, -56.85174851683467523 ) ) ;
#87218=FACE_OUTER_BOUND ( 'NONE', #87289, .T. ) ;
#87282=VERTEX_POINT ( 'NONE', #19162 ) ;
#87283=CARTESIAN_POINT ( 'NONE',  ( 9.797174393178825657E-16, -0.5000000000000000000, -8.000000000000000000 ) ) ;
#87289=EDGE_LOOP ( 'NONE', ( #11544, #27497, #71983, #36903 ) ) ;
#87321=CARTESIAN_POINT ( 'NONE',  ( 7.929588024479113465E-15, 50.00000000000000000, -64.50000000000000000 ) ) ;
#87405=COLOUR_RGB ( '', 0.72549020, 0.75294118, 0.79215686) ;
#87406=UNCERTAINTY_MEASURE_WITH_UNIT (LENGTH_MEASURE( 1.000000000000000082E-05 ), #16586, 'distance_accuracy_value', 'NONE');
#87426=( LENGTH_UNIT ( ) NAMED_UNIT ( * ) SI_UNIT ( .MILLI., .METRE. ) );
#87487=AXIS2_PLACEMENT_3D ( 'NONE', #97716, #70810, #55649 ) ;
#87613=CARTESIAN_POINT ( 'NONE',  ( 4.488554439770307297E-15, -1.341159125180006795, -15.80007993603364724 ) ) ;
#87661=FACE_OUTER_BOUND ( 'NONE', #106638, .T. ) ;
#87679=EDGE_CURVE ( 'NONE', #97678, #105636, #37073, .T. ) ;
#87694=LINE ( 'NONE', #12190, #15556 ) ;
#87713=DIRECTION ( 'NONE',  ( 0.000000000000000000, 1.000000000000000000, 0.000000000000000000 ) ) ;
#87742=FILL_AREA_STYLE ('',( #103903 ) ) ;
#87858=CIRCLE ( 'NONE', #20776, 57.50357696970299770 ) ;
#87922=ORIENTED_EDGE ( 'NONE', *, *, #86906, .F. ) ;
#87947=DIRECTION ( 'NONE',  ( 0.000000000000000000, 1.000000000000000000, 0.000000000000000000 ) ) ;
#87965=CONICAL_SURFACE ( 'NONE', #79325, 15.00000000000000000, 0.7509290623979402168 ) ;
#88006=DIRECTION ( 'NONE',  ( 0.000000000000000000, 1.000000000000000000, 0.000000000000000000 ) ) ;
#88013=SURFACE_STYLE_USAGE ( .BOTH. , #29804 ) ;
#88017=CARTESIAN_POINT ( 'NONE',  ( 1.040949779275250140E-15, -14.49999999999999822, 8.500000000000000000 ) ) ;
#88192=AXIS2_PLACEMENT_3D ( 'NONE', #29968, #30495, #62859 ) ;
#88195=DIRECTION ( 'NONE',  ( 0.000000000000000000, 0.000000000000000000, 1.000000000000000000 ) ) ;
#88226=DIRECTION ( 'NONE',  ( 0.000000000000000000, 0.000000000000000000, 1.000000000000000000 ) ) ;
#88329=MECHANICAL_DESIGN_GEOMETRIC_PRESENTATION_REPRESENTATION('',(#57337),#33210);
#88407=( GEOMETRIC_REPRESENTATION_CONTEXT ( 3 ) GLOBAL_UNCERTAINTY_ASSIGNED_CONTEXT ( ( #54546 ) ) GLOBAL_UNIT_ASSIGNED_CONTEXT ( ( #1217, #17983, #9859 ) ) REPRESENTATION_CONTEXT ( 'NONE', 'WORKASPACE' ) );
#88478=FILL_AREA_STYLE ('',( #38355 ) ) ;
#88509=CARTESIAN_POINT ( 'NONE',  ( 7.286648454926750781E-15, 45.50000000000000711, -59.50000000000000000 ) ) ;
#88544=TOROIDAL_SURFACE ( 'NONE', #93790, 65.50000000000000000, 0.5000000000000000000 ) ;
#88655=AXIS2_PLACEMENT_3D ( 'NONE', #10499, #75223, #26734 ) ;
#88702=DIRECTION ( 'NONE',  ( -1.000000000000000000, 0.000000000000000000, 0.000000000000000000 ) ) ;
#88705=CARTESIAN_POINT ( 'NONE',  ( 0.000000000000000000, -1.341159125180006795, 15.80007993603364724 ) ) ;
#88725=DIRECTION ( 'NONE',  ( 1.224646799147353454E-16, 0.000000000000000000, -1.000000000000000000 ) ) ;
#88760=CARTESIAN_POINT ( 'NONE',  ( 0.000000000000000000, 43.50000000000000711, 57.86910460382442523 ) ) ;
#88773=CIRCLE ( 'NONE', #40574, 66.00000000000000000 ) ;
#88832=CARTESIAN_POINT ( 'NONE',  ( 8.113285044351216187E-15, 48.50000000000000000, -66.00000000000000000 ) ) ;
#88849=CIRCLE ( 'NONE', #76745, 66.50000000000000000 ) ;
#88887=FILL_AREA_STYLE_COLOUR ( '', #51483 ) ;
#88931=DIRECTION ( 'NONE',  ( 0.000000000000000000, 0.000000000000000000, 1.000000000000000000 ) ) ;
#88962=DIRECTION ( 'NONE',  ( 0.000000000000000000, 0.000000000000000000, 1.000000000000000000 ) ) ;
#89048=UNCERTAINTY_MEASURE_WITH_UNIT (LENGTH_MEASURE( 1.000000000000000082E-05 ), #8046, 'distance_accuracy_value', 'NONE');
#89055=EDGE_CURVE ( 'NONE', #1507, #21338, #1660, .T. ) ;
#89117=CYLINDRICAL_SURFACE ( 'NONE', #87487, 9.500000000000000000 ) ;
#89124=ORIENTED_EDGE ( 'NONE', *, *, #98683, .T. ) ;
#89460=STYLED_ITEM ( 'NONE', ( #13027 ), #40448 ) ;
#89515=FILL_AREA_STYLE ('',( #55518 ) ) ;
#89573=ADVANCED_FACE ( 'NONE', ( #62497 ), #30142, .F. ) ;
#89656=EDGE_CURVE ( 'NONE', #8869, #54015, #15298, .T. ) ;
#89707=MANIFOLD_SOLID_BREP ( 'Fillet5', #72181 ) ;
#89804=VERTEX_POINT ( 'NONE', #59188 ) ;
#89884=EDGE_CURVE ( 'NONE', #43, #10331, #77284, .T. ) ;
#89909=CARTESIAN_POINT ( 'NONE',  ( 9.797174393178825657E-16, 0.000000000000000000, -8.000000000000000000 ) ) ;
#89925=ORIENTED_EDGE ( 'NONE', *, *, #47857, .F. ) ;
#89991=ORIENTED_EDGE ( 'NONE', *, *, #85692, .T. ) ;
#90008=VECTOR ( 'NONE', #79763, 1000.000000000000000 ) ;
#90071=DIRECTION ( 'NONE',  ( 0.000000000000000000, 0.000000000000000000, 1.000000000000000000 ) ) ;
#90121=EDGE_CURVE ( 'NONE', #99989, #75460, #49785, .T. ) ;
#90159=CARTESIAN_POINT ( 'NONE',  ( 0.000000000000000000, 0.000000000000000000, 8.000000000000000000 ) ) ;
#90178=AXIS2_PLACEMENT_3D ( 'NONE', #103741, #96717, #22324 ) ;
#90282=ORIENTED_EDGE ( 'NONE', *, *, #1198, .F. ) ;
#90307=EDGE_CURVE ( 'NONE', #84910, #80282, #20609, .T. ) ;
#90421=ORIENTED_EDGE ( 'NONE', *, *, #2232, .F. ) ;
#90561=ORIENTED_EDGE ( 'NONE', *, *, #17773, .F. ) ;
#90606=STYLED_ITEM ( 'NONE', ( #95407 ), #63990 ) ;
#90616=EDGE_CURVE ( 'NONE', #97678, #63571, #106605, .T. ) ;
#90673=EDGE_CURVE ( 'NONE', #38824, #50441, #67130, .T. ) ;
#90688=ORIENTED_EDGE ( 'NONE', *, *, #72104, .F. ) ;
#90977=DIRECTION ( 'NONE',  ( 0.000000000000000000, 0.000000000000000000, 1.000000000000000000 ) ) ;
#91256=DIRECTION ( 'NONE',  ( -0.000000000000000000, -1.000000000000000000, -0.000000000000000000 ) ) ;
#91332=AXIS2_PLACEMENT_3D ( 'NONE', #30579, #72593, #6256 ) ;
#91430=AXIS2_PLACEMENT_3D ( 'NONE', #4654, #101743, #45125 ) ;
#91493=UNCERTAINTY_MEASURE_WITH_UNIT (LENGTH_MEASURE( 1.000000000000000082E-05 ), #99651, 'distance_accuracy_value', 'NONE');
#91582=DIRECTION ( 'NONE',  ( 0.000000000000000000, 0.000000000000000000, 1.000000000000000000 ) ) ;
#91714=UNCERTAINTY_MEASURE_WITH_UNIT (LENGTH_MEASURE( 1.000000000000000082E-05 ), #85601, 'distance_accuracy_value', 'NONE');
#91719=EDGE_CURVE ( 'NONE', #62139, #15446, #77595, .T. ) ;
#91723=VERTEX_POINT ( 'NONE', #103118 ) ;
#91794=DIRECTION ( 'NONE',  ( 0.000000000000000000, 0.000000000000000000, 1.000000000000000000 ) ) ;
#91856=AXIS2_PLACEMENT_3D ( 'NONE', #49114, #78986, #38041 ) ;
#91875=ORIENTED_EDGE ( 'NONE', *, *, #53800, .F. ) ;
#92143=DIRECTION ( 'NONE',  ( -1.000000000000000000, 0.000000000000000000, 0.000000000000000000 ) ) ;
#92229=FACE_OUTER_BOUND ( 'NONE', #62964, .T. ) ;
#92254=CARTESIAN_POINT ( 'NONE',  ( 0.000000000000000000, 43.34115912517999902, 0.000000000000000000 ) ) ;
#92338=CIRCLE ( 'NONE', #47598, 10.00000000000000000 ) ;
#92481=CIRCLE ( 'NONE', #23612, 9.000000000000000000 ) ;
#92620=CIRCLE ( 'NONE', #68538, 66.50000000000000000 ) ;
#92669=VERTEX_POINT ( 'NONE', #49283 ) ;
#92684=CARTESIAN_POINT ( 'NONE',  ( 0.000000000000000000, 45.00000000000000711, 0.000000000000000000 ) ) ;
#92902=CARTESIAN_POINT ( 'NONE',  ( 0.000000000000000000, -14.49999999999999822, -8.500000000000000000 ) ) ;
#92911=FILL_AREA_STYLE_COLOUR ( '', #33301 ) ;
#92919=EDGE_CURVE ( 'NONE', #22823, #19286, #104752, .T. ) ;
#92968=DIRECTION ( 'NONE',  ( 0.000000000000000000, 0.000000000000000000, -1.000000000000000000 ) ) ;
#93012=DIRECTION ( 'NONE',  ( -1.000000000000000000, 0.000000000000000000, 0.000000000000000000 ) ) ;
#93094=DIRECTION ( 'NONE',  ( 0.000000000000000000, 1.000000000000000000, 0.000000000000000000 ) ) ;
#93144=SURFACE_STYLE_FILL_AREA ( #85057 ) ;
#93246=EDGE_CURVE ( 'NONE', #30956, #33490, #10594, .T. ) ;
#93293=AXIS2_PLACEMENT_3D ( 'NONE', #15606, #32359, #25333 ) ;
#93377=STYLED_ITEM ( 'NONE', ( #34937 ), #56232 ) ;
#93420=SURFACE_SIDE_STYLE ('',( #68628 ) ) ;
#93464=CARTESIAN_POINT ( 'NONE',  ( 0.000000000000000000, 45.50000000000000711, 60.00000000000000000 ) ) ;
#93514=EDGE_CURVE ( 'NONE', #1802, #9641, #82969, .T. ) ;
#93789=DIRECTION ( 'NONE',  ( 0.000000000000000000, 1.000000000000000000, 0.000000000000000000 ) ) ;
#93790=AXIS2_PLACEMENT_3D ( 'NONE', #27563, #66371, #11307 ) ;
#93854=AXIS2_PLACEMENT_3D ( 'NONE', #30407, #63296, #96194 ) ;
#93977=EDGE_CURVE ( 'NONE', #41058, #19286, #72712, .T. ) ;
#93992=PLANE ( 'NONE',  #40868 ) ;
#94149=AXIS2_PLACEMENT_3D ( 'NONE', #74303, #34431, #74827 ) ;
#94232=EDGE_CURVE ( 'NONE', #54015, #28073, #5592, .T. ) ;
#94251=VERTEX_POINT ( 'NONE', #59430 ) ;
#94288=FACE_OUTER_BOUND ( 'NONE', #11112, .T. ) ;
#94366=( GEOMETRIC_REPRESENTATION_CONTEXT ( 3 ) GLOBAL_UNCERTAINTY_ASSIGNED_CONTEXT ( ( #89048 ) ) GLOBAL_UNIT_ASSIGNED_CONTEXT ( ( #8046, #5921, #105162 ) ) REPRESENTATION_CONTEXT ( 'NONE', 'WORKASPACE' ) );
#94394=( GEOMETRIC_REPRESENTATION_CONTEXT ( 3 ) GLOBAL_UNCERTAINTY_ASSIGNED_CONTEXT ( ( #44913 ) ) GLOBAL_UNIT_ASSIGNED_CONTEXT ( ( #37370, #85354, #70235 ) ) REPRESENTATION_CONTEXT ( 'NONE', 'WORKASPACE' ) );
#94492=( NAMED_UNIT ( * ) SI_UNIT ( $, .STERADIAN. ) SOLID_ANGLE_UNIT ( ) );
#94524=ORIENTED_EDGE ( 'NONE', *, *, #21411, .T. ) ;
#94585=EDGE_CURVE ( 'NONE', #2579, #31239, #57310, .T. ) ;
#94792=EDGE_CURVE ( 'NONE', #60249, #106756, #21186, .T. ) ;
#94806=ORIENTED_EDGE ( 'NONE', *, *, #11565, .T. ) ;
#94867=CARTESIAN_POINT ( 'NONE',  ( 0.000000000000000000, -1.500000000000000000, -8.000000000000000000 ) ) ;
#94897=( NAMED_UNIT ( * ) SI_UNIT ( $, .STERADIAN. ) SOLID_ANGLE_UNIT ( ) );
#94935=SURFACE_SIDE_STYLE ('',( #6277 ) ) ;
#95006=ORIENTED_EDGE ( 'NONE', *, *, #70467, .F. ) ;
#95059=DIRECTION ( 'NONE',  ( 1.000000000000000000, 0.000000000000000000, -1.224646799147353207E-16 ) ) ;
#95091=PLANE ( 'NONE',  #26942 ) ;
#95136=DIRECTION ( 'NONE',  ( 0.000000000000000000, 0.000000000000000000, 1.000000000000000000 ) ) ;
#95167=DIRECTION ( 'NONE',  ( 0.000000000000000000, 0.000000000000000000, 1.000000000000000000 ) ) ;
#95213=CARTESIAN_POINT ( 'NONE',  ( 0.000000000000000000, 44.50000000000000711, 57.21727615095610275 ) ) ;
#95343=MECHANICAL_DESIGN_GEOMETRIC_PRESENTATION_REPRESENTATION('',(#38538),#52284);
#95349=ORIENTED_EDGE ( 'NONE', *, *, #57441, .F. ) ;
#95375=ORIENTED_EDGE ( 'NONE', *, *, #9834, .T. ) ;
#95381=CARTESIAN_POINT ( 'NONE',  ( 0.000000000000000000, -14.49999999999999822, -9.000000000000000000 ) ) ;
#95382=DIRECTION ( 'NONE',  ( 0.000000000000000000, 1.000000000000000000, 0.000000000000000000 ) ) ;
#95384=CARTESIAN_POINT ( 'NONE',  ( 0.000000000000000000, 48.50000000000000000, 62.00000000000000000 ) ) ;
#95390=ORIENTED_EDGE ( 'NONE', *, *, #21862, .T. ) ;
#95407=PRESENTATION_STYLE_ASSIGNMENT (( #28582 ) ) ;
#95525=DIRECTION ( 'NONE',  ( 0.000000000000000000, 1.000000000000000000, 0.000000000000000000 ) ) ;
#95596=ORIENTED_EDGE ( 'NONE', *, *, #17815, .T. ) ;
#95615=DIRECTION ( 'NONE',  ( 0.000000000000000000, 0.000000000000000000, 1.000000000000000000 ) ) ;
#95793=CIRCLE ( 'NONE', #28598, 0.5000000000000004441 ) ;
#95795=AXIS2_PLACEMENT_3D ( 'NONE', #103932, #68539, #85238 ) ;
#95829=( NAMED_UNIT ( * ) SI_UNIT ( $, .STERADIAN. ) SOLID_ANGLE_UNIT ( ) );
#95883=DIRECTION ( 'NONE',  ( 0.000000000000000000, 1.000000000000000000, 0.000000000000000000 ) ) ;
#95938=CARTESIAN_POINT ( 'NONE',  ( 0.000000000000000000, -15.00000000000000000, -8.500000000000000000 ) ) ;
#95951=( NAMED_UNIT ( * ) PLANE_ANGLE_UNIT ( ) SI_UNIT ( $, .RADIAN. ) );
#96000=CARTESIAN_POINT ( 'NONE',  ( 0.000000000000000000, 0.000000000000000000, 0.000000000000000000 ) ) ;
#96013=VERTEX_POINT ( 'NONE', #87321 ) ;
#96018=( GEOMETRIC_REPRESENTATION_CONTEXT ( 3 ) GLOBAL_UNCERTAINTY_ASSIGNED_CONTEXT ( ( #1680 ) ) GLOBAL_UNIT_ASSIGNED_CONTEXT ( ( #104797, #13651, #46041 ) ) REPRESENTATION_CONTEXT ( 'NONE', 'WORKASPACE' ) );
#96019=SURFACE_SIDE_STYLE ('',( #63118 ) ) ;
#96076=EDGE_LOOP ( 'NONE', ( #60098, #89124, #57555, #45431 ) ) ;
#96163=EDGE_LOOP ( 'NONE', ( #14542, #45494, #26593, #46573 ) ) ;
#96187=CARTESIAN_POINT ( 'NONE',  ( 1.224646799147353256E-15, -2.000000000000000000, -10.00000000000000000 ) ) ;
#96191=SURFACE_STYLE_USAGE ( .BOTH. , #29881 ) ;
#96194=DIRECTION ( 'NONE',  ( 0.000000000000000000, 0.000000000000000000, 1.000000000000000000 ) ) ;
#96245=MECHANICAL_DESIGN_GEOMETRIC_PRESENTATION_REPRESENTATION('',(#1497),#70449);
#96392=FACE_OUTER_BOUND ( 'NONE', #13043, .T. ) ;
#96444=CARTESIAN_POINT ( 'NONE',  ( 0.000000000000000000, 45.50000000000000711, 0.000000000000000000 ) ) ;
#96457=( NAMED_UNIT ( * ) SI_UNIT ( $, .STERADIAN. ) SOLID_ANGLE_UNIT ( ) );
#96569=CARTESIAN_POINT ( 'NONE',  ( 0.000000000000000000, 48.00000000000000000, 0.000000000000000000 ) ) ;
#96631=FILL_AREA_STYLE ('',( #72348 ) ) ;
#96717=DIRECTION ( 'NONE',  ( 0.000000000000000000, 1.000000000000000000, 0.000000000000000000 ) ) ;
#96798=DIRECTION ( 'NONE',  ( 0.000000000000000000, 0.000000000000000000, -1.000000000000000000 ) ) ;
#96883=PRESENTATION_STYLE_ASSIGNMENT (( #22500 ) ) ;
#96893=DIRECTION ( 'NONE',  ( -0.000000000000000000, -1.000000000000000000, -0.000000000000000000 ) ) ;
#96917=ORIENTED_EDGE ( 'NONE', *, *, #86906, .T. ) ;
#96938=CIRCLE ( 'NONE', #17720, 59.50000000000000000 ) ;
#96974=DIRECTION ( 'NONE',  ( 0.000000000000000000, 0.000000000000000000, 1.000000000000000000 ) ) ;
#96978=( NAMED_UNIT ( * ) PLANE_ANGLE_UNIT ( ) SI_UNIT ( $, .RADIAN. ) );
#97009=COLOUR_RGB ( '', 0.09019608, 0.27058824, 0.51372549) ;
#97081=SURFACE_SIDE_STYLE ('',( #5939 ) ) ;
#97211=PRESENTATION_STYLE_ASSIGNMENT (( #47063 ) ) ;
#97292=DIRECTION ( 'NONE',  ( 0.000000000000000000, 1.000000000000000000, 0.000000000000000000 ) ) ;
#97389=( NAMED_UNIT ( * ) PLANE_ANGLE_UNIT ( ) SI_UNIT ( $, .RADIAN. ) );
#97460=SURFACE_STYLE_USAGE ( .BOTH. , #80217 ) ;
#97483=DIRECTION ( 'NONE',  ( 0.000000000000000000, 0.000000000000000000, 1.000000000000000000 ) ) ;
#97520=CIRCLE ( 'NONE', #47635, 65.00000000000000000 ) ;
#97521=AXIS2_PLACEMENT_3D ( 'NONE', #92254, #17870, #50213 ) ;
#97560=FACE_OUTER_BOUND ( 'NONE', #102112, .T. ) ;
#97572=AXIS2_PLACEMENT_3D ( 'NONE', #42855, #11002, #84916 ) ;
#97658=FILL_AREA_STYLE_COLOUR ( '', #82522 ) ;
#97678=VERTEX_POINT ( 'NONE', #59186 ) ;
#97716=CARTESIAN_POINT ( 'NONE',  ( 0.000000000000000000, 0.000000000000000000, 0.000000000000000000 ) ) ;
#97776=DIRECTION ( 'NONE',  ( -0.000000000000000000, -1.000000000000000000, -0.000000000000000000 ) ) ;
#97780=VERTEX_POINT ( 'NONE', #99621 ) ;
#97851=CARTESIAN_POINT ( 'NONE',  ( 0.000000000000000000, 45.50000000000000711, 0.000000000000000000 ) ) ;
#97994=CARTESIAN_POINT ( 'NONE',  ( 0.000000000000000000, 79.50000000000000000, 0.000000000000000000 ) ) ;
#98033=EDGE_CURVE ( 'NONE', #37408, #22326, #48808, .T. ) ;
#98039=UNCERTAINTY_MEASURE_WITH_UNIT (LENGTH_MEASURE( 1.000000000000000082E-05 ), #4210, 'distance_accuracy_value', 'NONE');
#98156=AXIS2_PLACEMENT_3D ( 'NONE', #106606, #16541, #56451 ) ;
#98282=DIRECTION ( 'NONE',  ( 0.000000000000000000, 1.000000000000000000, 0.000000000000000000 ) ) ;
#98311=ADVANCED_FACE ( 'NONE', ( #78282 ), #86903, .F. ) ;
#98316=DIRECTION ( 'NONE',  ( -0.000000000000000000, -1.000000000000000000, -0.000000000000000000 ) ) ;
#98436=ADVANCED_FACE ( 'NONE', ( #63177 ), #55575, .F. ) ;
#98506=CARTESIAN_POINT ( 'NONE',  ( 0.000000000000000000, 50.00000000000000000, 64.50000000000000000 ) ) ;
#98532=DIRECTION ( 'NONE',  ( -0.000000000000000000, -1.000000000000000000, -0.000000000000000000 ) ) ;
#98549=CARTESIAN_POINT ( 'NONE',  ( 0.000000000000000000, -14.49999999999999822, 9.500000000000000000 ) ) ;
#98561=( LENGTH_UNIT ( ) NAMED_UNIT ( * ) SI_UNIT ( .MILLI., .METRE. ) );
#98601=DIRECTION ( 'NONE',  ( 0.000000000000000000, 0.000000000000000000, 1.000000000000000000 ) ) ;
#98683=EDGE_CURVE ( 'NONE', #30956, #31239, #74924, .T. ) ;
#98718=ORIENTED_EDGE ( 'NONE', *, *, #1113, .T. ) ;
#98723=ORIENTED_EDGE ( 'NONE', *, *, #50012, .F. ) ;
#98787=ORIENTED_EDGE ( 'NONE', *, *, #28265, .T. ) ;
#98926=ORIENTED_EDGE ( 'NONE', *, *, #70467, .T. ) ;
#98941=DIRECTION ( 'NONE',  ( 0.000000000000000000, 0.000000000000000000, 1.000000000000000000 ) ) ;
#98962=EDGE_CURVE ( 'NONE', #73621, #28073, #23232, .T. ) ;
#99005=CARTESIAN_POINT ( 'NONE',  ( 8.082668874372532400E-15, 79.50000000000000000, 66.00000000000000000 ) ) ;
#99037=DIRECTION ( 'NONE',  ( 0.000000000000000000, 0.000000000000000000, -1.000000000000000000 ) ) ;
#99153=ORIENTED_EDGE ( 'NONE', *, *, #90121, .F. ) ;
#99450=VECTOR ( 'NONE', #61921, 1000.000000000000114 ) ;
#99607=DIRECTION ( 'NONE',  ( 0.000000000000000000, 1.000000000000000000, 0.000000000000000000 ) ) ;
#99621=CARTESIAN_POINT ( 'NONE',  ( 7.317264624905434569E-15, 45.00000000000000711, -59.50000000000000000 ) ) ;
#99632=DIRECTION ( 'NONE',  ( 0.000000000000000000, 0.000000000000000000, 1.000000000000000000 ) ) ;
#99651=( LENGTH_UNIT ( ) NAMED_UNIT ( * ) SI_UNIT ( .MILLI., .METRE. ) );
#99655=DIRECTION ( 'NONE',  ( 0.000000000000000000, 1.000000000000000000, 0.000000000000000000 ) ) ;
#99682=ORIENTED_EDGE ( 'NONE', *, *, #32591, .F. ) ;
#99939=FACE_OUTER_BOUND ( 'NONE', #48441, .T. ) ;
#99983=ADVANCED_FACE ( 'NONE', ( #47164 ), #81126, .T. ) ;
#99989=VERTEX_POINT ( 'NONE', #88705 ) ;
#100022=EDGE_LOOP ( 'NONE', ( #25837, #2359 ) ) ;
#100085=ORIENTED_EDGE ( 'NONE', *, *, #46330, .T. ) ;
#100106=DIRECTION ( 'NONE',  ( 1.000000000000000000, 0.000000000000000000, -1.224646799147353207E-16 ) ) ;
#100237=EDGE_CURVE ( 'NONE', #10331, #1507, #100965, .T. ) ;
#100275=DIRECTION ( 'NONE',  ( 0.000000000000000000, 0.000000000000000000, 1.000000000000000000 ) ) ;
#100305=EDGE_CURVE ( 'NONE', #160, #60249, #92338, .T. ) ;
#100349=ORIENTED_EDGE ( 'NONE', *, *, #80730, .F. ) ;
#100352=FACE_OUTER_BOUND ( 'NONE', #85173, .T. ) ;
#100396=DIRECTION ( 'NONE',  ( -0.000000000000000000, -1.000000000000000000, -0.000000000000000000 ) ) ;
#100403=FACE_OUTER_BOUND ( 'NONE', #54582, .T. ) ;
#100557=EDGE_LOOP ( 'NONE', ( #42974, #23530, #8504, #100349 ) ) ;
#100563=ADVANCED_FACE ( 'NONE', ( #104749, #55638 ), #95091, .F. ) ;
#100633=CARTESIAN_POINT ( 'NONE',  ( 0.000000000000000000, 50.50000000000000000, 0.000000000000000000 ) ) ;
#100734=PRODUCT_DEFINITION_FORMATION_WITH_SPECIFIED_SOURCE ( 'ANY', '', #11294, .NOT_KNOWN. ) ;
#100899=CIRCLE ( 'NONE', #16522, 0.5000000000000004441 ) ;
#100917=UNCERTAINTY_MEASURE_WITH_UNIT (LENGTH_MEASURE( 1.000000000000000082E-05 ), #53990, 'distance_accuracy_value', 'NONE');
#100965=CIRCLE ( 'NONE', #52770, 0.5000000000000004441 ) ;
#101270=AXIS2_PLACEMENT_3D ( 'NONE', #6583, #21758, #95615 ) ;
#101306=EDGE_CURVE ( 'NONE', #7894, #15446, #1219, .T. ) ;
#101312=CARTESIAN_POINT ( 'NONE',  ( 1.040949779275250140E-15, -15.00000000000000000, 8.500000000000000000 ) ) ;
#101539=SURFACE_STYLE_USAGE ( .BOTH. , #52989 ) ;
#101743=DIRECTION ( 'NONE',  ( -0.000000000000000000, -1.000000000000000000, -0.000000000000000000 ) ) ;
#101757=CARTESIAN_POINT ( 'NONE',  ( 0.000000000000000000, 50.00000000000000000, 0.000000000000000000 ) ) ;
#101759=DIRECTION ( 'NONE',  ( 0.000000000000000000, 0.000000000000000000, -1.000000000000000000 ) ) ;
#101853=EDGE_CURVE ( 'NONE', #21929, #83020, #37573, .T. ) ;
#101956=MECHANICAL_DESIGN_GEOMETRIC_PRESENTATION_REPRESENTATION('',(#65844),#60655);
#102002=ORIENTED_EDGE ( 'NONE', *, *, #28265, .F. ) ;
#102109=STYLED_ITEM ( 'NONE', ( #97211 ), #20943 ) ;
#102112=EDGE_LOOP ( 'NONE', ( #83250, #42110, #30400, #85654 ) ) ;
#102119=CARTESIAN_POINT ( 'NONE',  ( 8.113285044351216187E-15, 80.00000000000000000, 66.00000000000000000 ) ) ;
#102256=ORIENTED_EDGE ( 'NONE', *, *, #73725, .T. ) ;
#102269=CARTESIAN_POINT ( 'NONE',  ( 0.000000000000000000, 50.00000000000000000, -60.00000000000000000 ) ) ;
#102283=ADVANCED_FACE ( 'NONE', ( #65864, #100352 ), #17866, .F. ) ;
#102380=DIRECTION ( 'NONE',  ( 1.000000000000000000, -0.000000000000000000, 1.224646799147353207E-16 ) ) ;
#102390=CIRCLE ( 'NONE', #31732, 0.5000000000000004441 ) ;
#102719=CARTESIAN_POINT ( 'NONE',  ( 8.021436534415164826E-15, 80.00000000000000000, 65.50000000000000000 ) ) ;
#102836=DIRECTION ( 'NONE',  ( -0.000000000000000000, -1.000000000000000000, -0.000000000000000000 ) ) ;
#102865=( NAMED_UNIT ( * ) PLANE_ANGLE_UNIT ( ) SI_UNIT ( $, .RADIAN. ) );
#102926=EDGE_LOOP ( 'NONE', ( #105413, #55761, #59533, #37169 ) ) ;
#102962=CARTESIAN_POINT ( 'NONE',  ( 0.000000000000000000, -15.00000000000000000, 0.000000000000000000 ) ) ;
#103005=CARTESIAN_POINT ( 'NONE',  ( 8.082668874372532400E-15, 49.00000000000000000, -66.00000000000000000 ) ) ;
#103047=EDGE_LOOP ( 'NONE', ( #19704, #6272, #65267, #37022 ) ) ;
#103118=CARTESIAN_POINT ( 'NONE',  ( 7.409113134841487507E-15, 50.00000000000000000, -60.50000000000000000 ) ) ;
#103135=DIRECTION ( 'NONE',  ( 0.000000000000000000, 0.000000000000000000, 1.000000000000000000 ) ) ;
#103150=DIRECTION ( 'NONE',  ( 0.000000000000000000, -1.000000000000000000, -0.000000000000000000 ) ) ;
#103218=SURFACE_SIDE_STYLE ('',( #70322 ) ) ;
#103222=CONICAL_SURFACE ( 'NONE', #39471, 16.09658290236430389, 0.7509290623979402168 ) ;
#103224=ORIENTED_EDGE ( 'NONE', *, *, #46459, .F. ) ;
#103300=AXIS2_PLACEMENT_3D ( 'NONE', #12852, #95382, #63562 ) ;
#103318=AXIS2_PLACEMENT_3D ( 'NONE', #29522, #86680, #77507 ) ;
#103321=UNCERTAINTY_MEASURE_WITH_UNIT (LENGTH_MEASURE( 1.000000000000000082E-05 ), #47253, 'distance_accuracy_value', 'NONE');
#103400=AXIS2_PLACEMENT_3D ( 'NONE', #76361, #93094, #26279 ) ;
#103402=TOROIDAL_SURFACE ( 'NONE', #91332, 8.500000000000000000, 0.5000000000000000000 ) ;
#103411=LINE ( 'NONE', #37659, #99450 ) ;
#103433=CARTESIAN_POINT ( 'NONE',  ( 0.000000000000000000, 44.00000000000000711, 0.000000000000000000 ) ) ;
#103469=DIRECTION ( 'NONE',  ( 0.000000000000000000, 0.000000000000000000, 1.000000000000000000 ) ) ;
#103543=EDGE_CURVE ( 'NONE', #9641, #84383, #31202, .T. ) ;
#103623=DIRECTION ( 'NONE',  ( 0.000000000000000000, 1.000000000000000000, 0.000000000000000000 ) ) ;
#103648=( NAMED_UNIT ( * ) SI_UNIT ( $, .STERADIAN. ) SOLID_ANGLE_UNIT ( ) );
#103655=( NAMED_UNIT ( * ) SI_UNIT ( $, .STERADIAN. ) SOLID_ANGLE_UNIT ( ) );
#103701=CARTESIAN_POINT ( 'NONE',  ( 8.021436534415164826E-15, 79.50000000000000000, 65.50000000000000000 ) ) ;
#103705=ORIENTED_EDGE ( 'NONE', *, *, #65236, .T. ) ;
#103721=ORIENTED_EDGE ( 'NONE', *, *, #19819, .F. ) ;
#103741=CARTESIAN_POINT ( 'NONE',  ( 0.000000000000000000, 49.00000000000000000, 0.000000000000000000 ) ) ;
#103874=CARTESIAN_POINT ( 'NONE',  ( 0.000000000000000000, -1.341159125180006795, 0.000000000000000000 ) ) ;
#103896=DIRECTION ( 'NONE',  ( 0.000000000000000000, 0.000000000000000000, -1.000000000000000000 ) ) ;
#103903=FILL_AREA_STYLE_COLOUR ( '', #82623 ) ;
#103932=CARTESIAN_POINT ( 'NONE',  ( 0.000000000000000000, -2.000000000000000000, 0.000000000000000000 ) ) ;
#103953=FILL_AREA_STYLE ('',( #71578 ) ) ;
#103964=FILL_AREA_STYLE ('',( #22020 ) ) ;
#104035=FACE_OUTER_BOUND ( 'NONE', #102926, .T. ) ;
#104176=( NAMED_UNIT ( * ) PLANE_ANGLE_UNIT ( ) SI_UNIT ( $, .RADIAN. ) );
#104244=FILL_AREA_STYLE ('',( #71345 ) ) ;
#104355=DIRECTION ( 'NONE',  ( -0.000000000000000000, -1.000000000000000000, -0.000000000000000000 ) ) ;
#104378=MECHANICAL_DESIGN_GEOMETRIC_PRESENTATION_REPRESENTATION('',(#90606),#7895);
#104394=VECTOR ( 'NONE', #81505, 1000.000000000000000 ) ;
#104398=ORIENTED_EDGE ( 'NONE', *, *, #85294, .T. ) ;
#104430=FACE_OUTER_BOUND ( 'NONE', #21158, .T. ) ;
#104439=FILL_AREA_STYLE ('',( #12772 ) ) ;
#104499=( LENGTH_UNIT ( ) NAMED_UNIT ( * ) SI_UNIT ( .MILLI., .METRE. ) );
#104523=CARTESIAN_POINT ( 'NONE',  ( 0.000000000000000000, -2.000000000000000000, 0.000000000000000000 ) ) ;
#104603=CYLINDRICAL_SURFACE ( 'NONE', #41077, 8.000000000000000000 ) ;
#104626=CARTESIAN_POINT ( 'NONE',  ( 0.000000000000000000, 49.00000000000000000, 66.00000000000000000 ) ) ;
#104675=AXIS2_PLACEMENT_3D ( 'NONE', #3617, #85063, #75896 ) ;
#104692=AXIS2_PLACEMENT_3D ( 'NONE', #44367, #10904, #103135 ) ;
#104695=TOROIDAL_SURFACE ( 'NONE', #40949, 57.21727615095610275, 0.5000000000000000000 ) ;
#104749=FACE_BOUND ( 'NONE', #62552, .T. ) ;
#104752=LINE ( 'NONE', #38455, #27907 ) ;
#104797=( LENGTH_UNIT ( ) NAMED_UNIT ( * ) SI_UNIT ( .MILLI., .METRE. ) );
#104799=CARTESIAN_POINT ( 'NONE',  ( 0.000000000000000000, 0.000000000000000000, 0.000000000000000000 ) ) ;
#104954=CARTESIAN_POINT ( 'NONE',  ( 0.000000000000000000, 0.000000000000000000, 66.50000000000000000 ) ) ;
#104976=DIRECTION ( 'NONE',  ( 0.000000000000000000, 0.000000000000000000, 1.000000000000000000 ) ) ;
#105017=DIRECTION ( 'NONE',  ( 0.000000000000000000, 0.000000000000000000, 1.000000000000000000 ) ) ;
#105061=EDGE_CURVE ( 'NONE', #10331, #43, #48609, .T. ) ;
#105162=( NAMED_UNIT ( * ) SI_UNIT ( $, .STERADIAN. ) SOLID_ANGLE_UNIT ( ) );
#105236=ORIENTED_EDGE ( 'NONE', *, *, #46330, .F. ) ;
#105299=COLOUR_RGB ( '', 0.72549020, 0.75294118, 0.79215686) ;
#105400=EDGE_CURVE ( 'NONE', #84383, #9641, #45190, .T. ) ;
#105413=ORIENTED_EDGE ( 'NONE', *, *, #92919, .F. ) ;
#105432=DIRECTION ( 'NONE',  ( -1.000000000000000000, 0.000000000000000000, 0.000000000000000000 ) ) ;
#105482=ADVANCED_FACE ( 'NONE', ( #23039 ), #24418, .T. ) ;
#105525=ORIENTED_EDGE ( 'NONE', *, *, #17773, .T. ) ;
#105636=VERTEX_POINT ( 'NONE', #8413 ) ;
#105859=VECTOR ( 'NONE', #27081, 1000.000000000000114 ) ;
#105926=FACE_OUTER_BOUND ( 'NONE', #15788, .T. ) ;
#105929=DIRECTION ( 'NONE',  ( 0.000000000000000000, 1.000000000000000000, 0.000000000000000000 ) ) ;
#106102=DIRECTION ( 'NONE',  ( 1.224646799147349509E-16, 0.000000000000000000, -1.000000000000000000 ) ) ;
#106107=PRESENTATION_STYLE_ASSIGNMENT (( #23641 ) ) ;
#106220=AXIS2_PLACEMENT_3D ( 'NONE', #44096, #42486, #76982 ) ;
#106234=CARTESIAN_POINT ( 'NONE',  ( 0.000000000000000000, -2.000000000000000000, 10.00000000000000000 ) ) ;
#106441=ORIENTED_EDGE ( 'NONE', *, *, #93977, .T. ) ;
#106494=ORIENTED_EDGE ( 'NONE', *, *, #90616, .T. ) ;
#106598=EDGE_CURVE ( 'NONE', #1084, #92669, #31410, .T. ) ;
#106605=CIRCLE ( 'NONE', #60150, 62.00000000000000000 ) ;
#106606=CARTESIAN_POINT ( 'NONE',  ( 0.000000000000000000, 0.000000000000000000, 0.000000000000000000 ) ) ;
#106631=ORIENTED_EDGE ( 'NONE', *, *, #78732, .F. ) ;
#106638=EDGE_LOOP ( 'NONE', ( #50874, #59272, #34242, #81842 ) ) ;
#106653=PRESENTATION_STYLE_ASSIGNMENT (( #16591 ) ) ;
#106676=CARTESIAN_POINT ( 'NONE',  ( 0.000000000000000000, 80.00000000000000000, -65.50000000000000000 ) ) ;
#106716=ORIENTED_EDGE ( 'NONE', *, *, #65794, .F. ) ;
#106756=VERTEX_POINT ( 'NONE', #72644 ) ;
ENDSEC;
END-ISO-10303-21;
